ISO-10303-21;
HEADER;
FILE_DESCRIPTION (('STEP AP214'),
    '1' );
FILE_NAME ('Cover Plate.step',
    '2026-10-06T13:23:30',
    ( '' ),
    ( '' ),
    'SwSTEP 2.0',
    'SolidWorks 2020',
    '' );
FILE_SCHEMA (( 'AUTOMOTIVE_DESIGN' ));
ENDSEC;

DATA;
#12=LINE ( 'NONE', #7259, #31 ) ;
#21=CARTESIAN_POINT ( 'NONE',  ( -13.53805010459570823, -42.60941606008491789, -136.0552959529695158 ) ) ;
#31=VECTOR ( 'NONE', #17982, 1000.000000000000000 ) ;
#32=VECTOR ( 'NONE', #119, 1000.000000000000000 ) ;
#33=DIRECTION ( 'NONE',  ( -2.257144641399999941E-12, 0.000000000000000000, -1.000000000000000000 ) ) ;
#44=ORIENTED_EDGE ( 'NONE', *, *, #15140, .T. ) ;
#52=ORIENTED_EDGE ( 'NONE', *, *, #9220, .T. ) ;
#57=EDGE_CURVE ( 'NONE', #16606, #2360, #10514, .T. ) ;
#86=CARTESIAN_POINT ( 'NONE',  ( 15.50000000000000000, 39.50000000000000000, -136.0552959530000123 ) ) ;
#88=DIRECTION ( 'NONE',  ( 2.257749542879999954E-12, 0.000000000000000000, 1.000000000000000000 ) ) ;
#89=ORIENTED_EDGE ( 'NONE', *, *, #22160, .F. ) ;
#92=DIRECTION ( 'NONE',  ( -2.257144641399999941E-12, 8.049635416090000264E-35, -1.000000000000000000 ) ) ;
#95=ORIENTED_EDGE ( 'NONE', *, *, #4265, .F. ) ;
#99=EDGE_CURVE ( 'NONE', #3836, #1507, #11570, .T. ) ;
#110=CARTESIAN_POINT ( 'NONE',  ( -25.86630785129999666, -51.50000000000000000, -136.5552959530000123 ) ) ;
#119=DIRECTION ( 'NONE',  ( -1.000000000000000000, 0.000000000000000000, 2.245315044999999693E-12 ) ) ;
#127=EDGE_CURVE ( 'NONE', #16762, #17721, #6116, .T. ) ;
#137=ORIENTED_EDGE ( 'NONE', *, *, #3234, .F. ) ;
#142=CARTESIAN_POINT ( 'NONE',  ( -13.80049973640272931, -43.92182007996237303, -136.0552959530027124 ) ) ;
#143=EDGE_LOOP ( 'NONE', ( #7087, #11554, #3660, #16017 ) ) ;
#148=ORIENTED_EDGE ( 'NONE', *, *, #4162, .F. ) ;
#149=CARTESIAN_POINT ( 'NONE',  ( 5.420128080818026106, -2.298969449354696604, -136.0552959530122337 ) ) ;
#158=CARTESIAN_POINT ( 'NONE',  ( 9.295843182404178506, -32.13416640351051967, -136.0552959530209876 ) ) ;
#165=ORIENTED_EDGE ( 'NONE', *, *, #16079, .F. ) ;
#178=CARTESIAN_POINT ( 'NONE',  ( -1.499999999960000219, 44.50000000000000000, -136.0552959530000123 ) ) ;
#181=ORIENTED_EDGE ( 'NONE', *, *, #506, .F. ) ;
#192=CARTESIAN_POINT ( 'NONE',  ( 31.50000000000000000, 36.50000000000000000, -137.0552959530000123 ) ) ;
#199=EDGE_CURVE ( 'NONE', #11395, #18017, #9780, .T. ) ;
#219=CARTESIAN_POINT ( 'NONE',  ( -13.86630785130000021, 51.50000000000000000, -136.5552959530000123 ) ) ;
#226=DIRECTION ( 'NONE',  ( 0.000000000000000000, 1.000000000000000000, 0.000000000000000000 ) ) ;
#234=CARTESIAN_POINT ( 'NONE',  ( 3.611688725869999975E-11, 34.00000000000000000, -136.0552959530000123 ) ) ;
#237=ORIENTED_EDGE ( 'NONE', *, *, #19571, .F. ) ;
#247=ORIENTED_EDGE ( 'NONE', *, *, #12729, .T. ) ;
#248=( NAMED_UNIT ( * ) SI_UNIT ( $, .STERADIAN. ) SOLID_ANGLE_UNIT ( ) );
#262=DIRECTION ( 'NONE',  ( 0.000000000000000000, 1.000000000000000000, 0.000000000000000000 ) ) ;
#268=CARTESIAN_POINT ( 'NONE',  ( 12.88103053862586478, 34.98519100497017575, -136.0552959530290593 ) ) ;
#274=CARTESIAN_POINT ( 'NONE',  ( 7.750000000030000002, -37.98606797749999942, -136.5552959530000123 ) ) ;
#293=CARTESIAN_POINT ( 'NONE',  ( -16.50000000000000000, -43.00000000000000000, -136.0552959530000123 ) ) ;
#305=CARTESIAN_POINT ( 'NONE',  ( 3.611688725869999975E-11, -37.98606797749999942, -136.0552959530000123 ) ) ;
#308=DIRECTION ( 'NONE',  ( 2.257144641397284947E-12, 2.714724913984255017E-24, 1.000000000000000000 ) ) ;
#318=ORIENTED_EDGE ( 'NONE', *, *, #17684, .T. ) ;
#339=CARTESIAN_POINT ( 'NONE',  ( 22.50000000000000000, 33.50000000000000000, -137.0552959530000123 ) ) ;
#375=VECTOR ( 'NONE', #11766, 1000.000000000000000 ) ;
#376=EDGE_LOOP ( 'NONE', ( #19580, #5131, #12195, #4247 ) ) ;
#379=CARTESIAN_POINT ( 'NONE',  ( 5.809749477036856291, -2.742473698248191649, -136.0552959530131432 ) ) ;
#396=DIRECTION ( 'NONE',  ( 2.257157423930000049E-12, 0.000000000000000000, 1.000000000000000000 ) ) ;
#398=VECTOR ( 'NONE', #22428, 1000.000000000000000 ) ;
#407=DIRECTION ( 'NONE',  ( 0.000000000000000000, 1.000000000000000000, 0.000000000000000000 ) ) ;
#415=DIRECTION ( 'NONE',  ( 2.259525899719999991E-12, 0.000000000000000000, 1.000000000000000000 ) ) ;
#416=VERTEX_POINT ( 'NONE', #16342 ) ;
#417=EDGE_CURVE ( 'NONE', #16549, #12948, #12397, .T. ) ;
#435=DIRECTION ( 'NONE',  ( 0.000000000000000000, 1.603797727410000024E-26, -1.000000000000000000 ) ) ;
#444=ORIENTED_EDGE ( 'NONE', *, *, #1007, .T. ) ;
#492=CARTESIAN_POINT ( 'NONE',  ( -5.499999999960005326, 44.23441892295438294, -136.0552959529876205 ) ) ;
#493=ORIENTED_EDGE ( 'NONE', *, *, #2717, .F. ) ;
#495=CARTESIAN_POINT ( 'NONE',  ( -15.39067985669018235, -44.46175622020449225, -136.0552959529652526 ) ) ;
#500=AXIS2_PLACEMENT_3D ( 'NONE', #8679, #15962, #22989 ) ;
#506=EDGE_CURVE ( 'NONE', #3901, #16131, #13345, .T. ) ;
#524=EDGE_CURVE ( 'NONE', #12078, #6964, #6093, .T. ) ;
#527=ORIENTED_EDGE ( 'NONE', *, *, #524, .F. ) ;
#532=LINE ( 'NONE', #16579, #17364 ) ;
#546=VERTEX_POINT ( 'NONE', #2424 ) ;
#559=ORIENTED_EDGE ( 'NONE', *, *, #6683, .T. ) ;
#564=LINE ( 'NONE', #18409, #4525 ) ;
#587=DIRECTION ( 'NONE',  ( 1.000000000000000000, 0.000000000000000000, -2.257120985840000117E-12 ) ) ;
#592=B_SPLINE_CURVE_WITH_KNOTS ( 'NONE', 3,
 ( #5537, #12672, #3987, #14821, #23392, #9212, #11220, #12786, #18494, #18153, #10755, #16137, #18038, #20057, #8972, #21737, #5427, #19939 ),
 .UNSPECIFIED., .F., .F.,
 ( 4, 2, 2, 2, 2, 2, 2, 2, 4 ),
 ( 0.000000000000000000, 0.1249999999999998057, 0.2499999999999998335, 0.3749999999999998335, 0.4999999999999998890, 0.6249999999999998890, 0.7499999999999998890, 0.8750000000000000000, 1.000000000000000000 ),
 .UNSPECIFIED. ) ;
#597=DIRECTION ( 'NONE',  ( 1.000000000000000000, -2.312964634635743450E-15, -2.257453483404485639E-12 ) ) ;
#600=VECTOR ( 'NONE', #18376, 1000.000000000000000 ) ;
#608=EDGE_CURVE ( 'NONE', #14496, #2454, #1959, .T. ) ;
#611=CARTESIAN_POINT ( 'NONE',  ( 5.701130924195719096, -2.579771545651550646, -136.0552959530129158 ) ) ;
#612=LINE ( 'NONE', #730, #5551 ) ;
#616=ORIENTED_EDGE ( 'NONE', *, *, #4162, .T. ) ;
#620=EDGE_CURVE ( 'NONE', #20642, #4666, #18468, .T. ) ;
#624=LINE ( 'NONE', #7513, #10296 ) ;
#631=CARTESIAN_POINT ( 'NONE',  ( -6.366307851350000213, -50.50000000000000000, -136.0552959530000123 ) ) ;
#633=EDGE_CURVE ( 'NONE', #11242, #11916, #16457, .T. ) ;
#639=PLANE ( 'NONE',  #16943 ) ;
#644=DIRECTION ( 'NONE',  ( 0.000000000000000000, -1.000000000000000000, 0.000000000000000000 ) ) ;
#662=FACE_BOUND ( 'NONE', #2795, .T. ) ;
#666=CARTESIAN_POINT ( 'NONE',  ( 32.50000000000000000, -40.50000000000000000, -137.0552959530000123 ) ) ;
#677=ORIENTED_EDGE ( 'NONE', *, *, #6323, .T. ) ;
#683=VERTEX_POINT ( 'NONE', #9754 ) ;
#697=CARTESIAN_POINT ( 'NONE',  ( 3.000000000010000001, -3.500000000000000000, -136.0552959530000123 ) ) ;
#706=DIRECTION ( 'NONE',  ( 1.000000000000000000, 0.000000000000000000, -2.257453483404485639E-12 ) ) ;
#717=ORIENTED_EDGE ( 'NONE', *, *, #2283, .F. ) ;
#721=CARTESIAN_POINT ( 'NONE',  ( -5.101575545643076026, 43.27312978694624945, -136.0552959529885015 ) ) ;
#730=CARTESIAN_POINT ( 'NONE',  ( 31.50000000000000000, -21.03620104879999886, -136.5552959530000123 ) ) ;
#738=VECTOR ( 'NONE', #14054, 1000.000000000000000 ) ;
#750=AXIS2_PLACEMENT_3D ( 'NONE', #14418, #16324, #33 ) ;
#782=ORIENTED_EDGE ( 'NONE', *, *, #7514, .F. ) ;
#785=CARTESIAN_POINT ( 'NONE',  ( 8.250000000030000891, -37.98606797749999942, -136.0552959530000123 ) ) ;
#795=EDGE_LOOP ( 'NONE', ( #318, #13967, #2520, #17759 ) ) ;
#805=DIRECTION ( 'NONE',  ( -1.000000000000000000, 0.000000000000000000, 2.257423253620000194E-12 ) ) ;
#824=VERTEX_POINT ( 'NONE', #5124 ) ;
#825=VECTOR ( 'NONE', #18383, 1000.000000000000000 ) ;
#829=DIRECTION ( 'NONE',  ( -2.257144641399999941E-12, 0.000000000000000000, -1.000000000000000000 ) ) ;
#839=ORIENTED_EDGE ( 'NONE', *, *, #2461, .T. ) ;
#851=CARTESIAN_POINT ( 'NONE',  ( -9.999999999959999997, 19.50000000000000000, -136.0552959530000123 ) ) ;
#873=DIRECTION ( 'NONE',  ( 0.000000000000000000, -1.000000000000000000, 0.000000000000000000 ) ) ;
#877=DIRECTION ( 'NONE',  ( -2.257144641399999941E-12, 8.049635416090000264E-35, -1.000000000000000000 ) ) ;
#878=ORIENTED_EDGE ( 'NONE', *, *, #3986, .T. ) ;
#880=DIRECTION ( 'NONE',  ( -1.000000000000000000, 5.094701932209999624E-24, 2.257144641399999941E-12 ) ) ;
#886=DIRECTION ( 'NONE',  ( 2.257749542879999954E-12, 0.000000000000000000, 1.000000000000000000 ) ) ;
#897=DIRECTION ( 'NONE',  ( -1.000000000000000000, 5.094701932209999624E-24, 2.257144641399999941E-12 ) ) ;
#905=EDGE_CURVE ( 'NONE', #11614, #16880, #2022, .T. ) ;
#907=EDGE_CURVE ( 'NONE', #3556, #4774, #9244, .T. ) ;
#910=VECTOR ( 'NONE', #8859, 1000.000000000000000 ) ;
#920=LINE ( 'NONE', #8145, #8728 ) ;
#921=ORIENTED_EDGE ( 'NONE', *, *, #10976, .T. ) ;
#931=DIRECTION ( 'NONE',  ( 1.000000000000000000, 0.000000000000000000, -2.257453483404485639E-12 ) ) ;
#939=EDGE_LOOP ( 'NONE', ( #4957, #18808, #12429, #12764 ) ) ;
#950=EDGE_LOOP ( 'NONE', ( #4953, #19405, #13964, #10896 ) ) ;
#951=CARTESIAN_POINT ( 'NONE',  ( 3.611688725869999975E-11, -51.50000000000000000, -136.0552959530000123 ) ) ;
#965=LINE ( 'NONE', #22723, #3243 ) ;
#991=CARTESIAN_POINT ( 'NONE',  ( -32.50000000000000000, 51.50000000000000000, -137.0552959530000123 ) ) ;
#1007=EDGE_CURVE ( 'NONE', #5202, #6635, #17208, .T. ) ;
#1016=DIRECTION ( 'NONE',  ( 0.7071067811865475727, -0.7071067811865475727, -1.595020412044807153E-12 ) ) ;
#1031=CARTESIAN_POINT ( 'NONE',  ( -7.499999999959999997, -2.273736754430000208E-12, -136.0552959530000123 ) ) ;
#1033=ADVANCED_FACE ( 'NONE', ( #8037 ), #11249, .T. ) ;
#1034=CARTESIAN_POINT ( 'NONE',  ( 22.50000000000000000, 39.50000000000000000, -137.0552959530000123 ) ) ;
#1036=CARTESIAN_POINT ( 'NONE',  ( -0.2409605966616616968, 23.82477348803141837, -136.0552959529995007 ) ) ;
#1054=DIRECTION ( 'NONE',  ( 1.000000000000000000, -5.094701932209999624E-24, -2.257144641399999941E-12 ) ) ;
#1055=CIRCLE ( 'NONE', #14350, 1.499999999999999556 ) ;
#1079=VECTOR ( 'NONE', #4853, 1000.000000000000000 ) ;
#1087=LINE ( 'NONE', #2519, #375 ) ;
#1089=CARTESIAN_POINT ( 'NONE',  ( -16.30994315220291213, -42.24256961503859031, -136.0552959529631778 ) ) ;
#1091=VECTOR ( 'NONE', #21185, 1000.000000000000000 ) ;
#1094=CARTESIAN_POINT ( 'NONE',  ( 15.10199673425556455, 39.50000000000002842, -136.0552959530340615 ) ) ;
#1111=DIRECTION ( 'NONE',  ( -2.257144641399999941E-12, 8.049635416090000264E-35, -1.000000000000000000 ) ) ;
#1112=VECTOR ( 'NONE', #3564, 1000.000000000000000 ) ;
#1115=DIRECTION ( 'NONE',  ( 2.257157423930000049E-12, 0.000000000000000000, 1.000000000000000000 ) ) ;
#1131=DIRECTION ( 'NONE',  ( 2.257144641399999941E-12, -8.049635416090000264E-35, 1.000000000000000000 ) ) ;
#1138=FACE_OUTER_BOUND ( 'NONE', #8262, .T. ) ;
#1139=VECTOR ( 'NONE', #23042, 1000.000000000000000 ) ;
#1142=FACE_OUTER_BOUND ( 'NONE', #8260, .T. ) ;
#1150=DIRECTION ( 'NONE',  ( 2.257144641397284947E-12, -2.714590281723094849E-24, 1.000000000000000000 ) ) ;
#1158=ORIENTED_EDGE ( 'NONE', *, *, #16087, .F. ) ;
#1161=DIRECTION ( 'NONE',  ( 1.000000000000000000, 0.000000000000000000, 0.000000000000000000 ) ) ;
#1165=CARTESIAN_POINT ( 'NONE',  ( 0.5374248537463910402, 25.07581004119176171, -136.0552959530012060 ) ) ;
#1173=AXIS2_PLACEMENT_3D ( 'NONE', #8912, #5236, #3339 ) ;
#1183=ORIENTED_EDGE ( 'NONE', *, *, #4487, .T. ) ;
#1184=DIRECTION ( 'NONE',  ( 1.000000000000000000, -5.094701932209999624E-24, -2.257144641399999941E-12 ) ) ;
#1216=DIRECTION ( 'NONE',  ( 1.000000000000000000, -5.094701932209999624E-24, 0.000000000000000000 ) ) ;
#1222=CARTESIAN_POINT ( 'NONE',  ( -15.00000000000000000, -43.00000000000000000, -137.0552959530000123 ) ) ;
#1230=CARTESIAN_POINT ( 'NONE',  ( 3.611688725869999975E-11, -50.50000000000000000, -136.0552959530000123 ) ) ;
#1234=CARTESIAN_POINT ( 'NONE',  ( 3.611688725869999975E-11, 20.96379895120000114, -136.0552959530000123 ) ) ;
#1239=EDGE_CURVE ( 'NONE', #16039, #2454, #13379, .T. ) ;
#1242=VERTEX_POINT ( 'NONE', #22082 ) ;
#1243=AXIS2_PLACEMENT_3D ( 'NONE', #5508, #19671, #7170 ) ;
#1245=DIRECTION ( 'NONE',  ( 5.094701932209999624E-24, 1.000000000000000000, -1.149947916579999802E-35 ) ) ;
#1246=LINE ( 'NONE', #17642, #21560 ) ;
#1253=ORIENTED_EDGE ( 'NONE', *, *, #20561, .T. ) ;
#1266=EDGE_CURVE ( 'NONE', #18017, #12077, #18743, .T. ) ;
#1270=CARTESIAN_POINT ( 'NONE',  ( 7.270619713791125704, -46.69911951120823090, -136.0552959530163832 ) ) ;
#1275=CARTESIAN_POINT ( 'NONE',  ( -3.499999999969999998, 42.50000000000000000, -136.5552959530000123 ) ) ;
#1277=DIRECTION ( 'NONE',  ( -1.000000000000000000, 5.094701932209999624E-24, 0.000000000000000000 ) ) ;
#1282=CARTESIAN_POINT ( 'NONE',  ( 4.554119375355614174, 27.76008370043819795, -136.0552959530103294 ) ) ;
#1284=ORIENTED_EDGE ( 'NONE', *, *, #17779, .T. ) ;
#1285=EDGE_CURVE ( 'NONE', #18664, #7623, #16593, .T. ) ;
#1297=CARTESIAN_POINT ( 'NONE',  ( 5.810679582541388832, -4.255428470556350540, -136.0552959530029682 ) ) ;
#1302=LINE ( 'NONE', #21401, #6387 ) ;
#1306=DIRECTION ( 'NONE',  ( 1.000000000000000000, -5.094701932209999624E-24, 0.000000000000000000 ) ) ;
#1311=ORIENTED_EDGE ( 'NONE', *, *, #15794, .F. ) ;
#1321=CARTESIAN_POINT ( 'NONE',  ( -1.550733472753473619, 45.02071668630011203, -136.0552959529965165 ) ) ;
#1332=DIRECTION ( 'NONE',  ( 2.257157423930000049E-12, 0.000000000000000000, 1.000000000000000000 ) ) ;
#1339=ADVANCED_FACE ( 'NONE', ( #9672 ), #18852, .T. ) ;
#1342=DIRECTION ( 'NONE',  ( 1.000000000000000000, 0.000000000000000000, -2.257453483404482811E-12 ) ) ;
#1346=PLANE ( 'NONE',  #12894 ) ;
#1353=ORIENTED_EDGE ( 'NONE', *, *, #15122, .T. ) ;
#1359=VERTEX_POINT ( 'NONE', #3990 ) ;
#1362=ADVANCED_FACE ( 'NONE', ( #11224 ), #18497, .T. ) ;
#1368=VECTOR ( 'NONE', #16491, 1000.000000000000000 ) ;
#1374=CARTESIAN_POINT ( 'NONE',  ( 4.750000000030004443, -45.01539404905023645, -136.0552959530107273 ) ) ;
#1387=VERTEX_POINT ( 'NONE', #19325 ) ;
#1416=CARTESIAN_POINT ( 'NONE',  ( -6.366307851350000213, 50.50000000000000000, -136.0552959530000123 ) ) ;
#1435=CARTESIAN_POINT ( 'NONE',  ( -5.499999999969999109, 44.50000000000000000, -137.0552959530000123 ) ) ;
#1437=CARTESIAN_POINT ( 'NONE',  ( 1.133692148650000009, -51.50000000000000000, -136.0552959530000123 ) ) ;
#1442=ORIENTED_EDGE ( 'NONE', *, *, #10525, .T. ) ;
#1451=CARTESIAN_POINT ( 'NONE',  ( -13.79886907581265909, -42.07977154562041733, -136.0552959529688621 ) ) ;
#1477=CARTESIAN_POINT ( 'NONE',  ( 5.298801200344347428, -31.10703351611365974, -136.0552959530119779 ) ) ;
#1482=CARTESIAN_POINT ( 'NONE',  ( 32.50000000000000000, -33.03620104880000241, -136.5552959530000123 ) ) ;
#1495=LINE ( 'NONE', #12529, #7921 ) ;
#1500=DIRECTION ( 'NONE',  ( 2.256861364460000137E-12, 0.000000000000000000, 1.000000000000000000 ) ) ;
#1504=CARTESIAN_POINT ( 'NONE',  ( 6.500000000030000002, 20.50000000000000000, -137.0552959530000123 ) ) ;
#1507=VERTEX_POINT ( 'NONE', #1728 ) ;
#1511=SURFACE_STYLE_FILL_AREA ( #12196 ) ;
#1521=LINE ( 'NONE', #3403, #3341 ) ;
#1522=VERTEX_POINT ( 'NONE', #1615 ) ;
#1525=EDGE_CURVE ( 'NONE', #11936, #12077, #12293, .T. ) ;
#1530=DIRECTION ( 'NONE',  ( 2.257144641397284947E-12, -2.714760815920564689E-24, 1.000000000000000000 ) ) ;
#1558=ADVANCED_FACE ( 'NONE', ( #3498 ), #8948, .F. ) ;
#1570=CARTESIAN_POINT ( 'NONE',  ( 6.007375567817776485, 13.00000000000000533, -136.0552959530135695 ) ) ;
#1577=SURFACE_STYLE_USAGE ( .BOTH. , #19998 ) ;
#1592=ORIENTED_EDGE ( 'NONE', *, *, #20615, .F. ) ;
#1606=CARTESIAN_POINT ( 'NONE',  ( 17.50006728700661540, 22.10251055748693005, -136.0552959530394901 ) ) ;
#1615=CARTESIAN_POINT ( 'NONE',  ( 8.750000000030000891, -35.98606797749999942, -137.0552959530000123 ) ) ;
#1616=( GEOMETRIC_REPRESENTATION_CONTEXT ( 3 ) GLOBAL_UNCERTAINTY_ASSIGNED_CONTEXT ( ( #16365 ) ) GLOBAL_UNIT_ASSIGNED_CONTEXT ( ( #10401, #21140, #19583 ) ) REPRESENTATION_CONTEXT ( 'NONE', 'WORKASPACE' ) );
#1618=ORIENTED_EDGE ( 'NONE', *, *, #12855, .F. ) ;
#1622=CARTESIAN_POINT ( 'NONE',  ( -12.50000000000000000, 48.50000000000000000, -136.0552959530000123 ) ) ;
#1630=ORIENTED_EDGE ( 'NONE', *, *, #3766, .T. ) ;
#1643=EDGE_CURVE ( 'NONE', #4170, #6635, #15991, .T. ) ;
#1644=CARTESIAN_POINT ( 'NONE',  ( 7.750000000030000002, -38.98606797749999942, -136.0552959530000123 ) ) ;
#1646=CARTESIAN_POINT ( 'NONE',  ( -3.499999999959999997, 44.50000000000000000, -136.0552959530000123 ) ) ;
#1656=DIRECTION ( 'NONE',  ( 2.257157423930000049E-12, 0.000000000000000000, 1.000000000000000000 ) ) ;
#1669=EDGE_CURVE ( 'NONE', #13712, #5167, #17729, .T. ) ;
#1671=CARTESIAN_POINT ( 'NONE',  ( 20.50000000000000000, 25.50000000000000000, -136.5552959530000123 ) ) ;
#1683=CARTESIAN_POINT ( 'NONE',  ( -0.6176558849126000394, 18.08432684250925959, -136.0552959529985628 ) ) ;
#1693=CARTESIAN_POINT ( 'NONE',  ( -3.499999999969999998, 40.00000000000000000, -137.0552959530000123 ) ) ;
#1703=ADVANCED_FACE ( 'NONE', ( #5115 ), #23091, .T. ) ;
#1710=ORIENTED_EDGE ( 'NONE', *, *, #9734, .T. ) ;
#1715=CARTESIAN_POINT ( 'NONE',  ( 9.593637377617811879, -34.75248504027396024, -136.0552959530216413 ) ) ;
#1716=VECTOR ( 'NONE', #14645, 1000.000000000000000 ) ;
#1725=CARTESIAN_POINT ( 'NONE',  ( -5.660514123294832167, 20.09808825513981034, -136.0552959529872510 ) ) ;
#1728=CARTESIAN_POINT ( 'NONE',  ( 13.13369214870000157, -50.50000000000000000, -136.0552959530000123 ) ) ;
#1738=LINE ( 'NONE', #1275, #12013 ) ;
#1740=DIRECTION ( 'NONE',  ( -2.257144641399999941E-12, 0.000000000000000000, -1.000000000000000000 ) ) ;
#1743=EDGE_LOOP ( 'NONE', ( #18864, #2469, #148, #16701 ) ) ;
#1749=AXIS2_PLACEMENT_3D ( 'NONE', #16844, #11581, #15406 ) ;
#1756=VERTEX_POINT ( 'NONE', #20111 ) ;
#1757=FACE_BOUND ( 'NONE', #16609, .T. ) ;
#1777=ORIENTED_EDGE ( 'NONE', *, *, #15799, .T. ) ;
#1805=PRODUCT_DEFINITION ( 'UNKNOWN', '', #21032, #4949 ) ;
#1830=CARTESIAN_POINT ( 'NONE',  ( 9.167789811918616749, -35.55184220689274355, -136.0552959530206749 ) ) ;
#1832=VECTOR ( 'NONE', #10189, 1000.000000000000000 ) ;
#1842=DIRECTION ( 'NONE',  ( 0.000000000000000000, 1.000000000000000000, 0.000000000000000000 ) ) ;
#1850=DIRECTION ( 'NONE',  ( -1.000000000000000000, 0.000000000000000000, 2.257120985840000117E-12 ) ) ;
#1853=EDGE_CURVE ( 'NONE', #16606, #15863, #6856, .T. ) ;
#1857=CARTESIAN_POINT ( 'NONE',  ( -3.499999999959999997, 42.50000000000000000, -136.0552959530000123 ) ) ;
#1866=ORIENTED_EDGE ( 'NONE', *, *, #3854, .T. ) ;
#1878=EDGE_CURVE ( 'NONE', #23163, #683, #12, .T. ) ;
#1883=EDGE_LOOP ( 'NONE', ( #2656, #6930, #13439, #15350 ) ) ;
#1888=CARTESIAN_POINT ( 'NONE',  ( 20.50000000000000000, 25.50000000000000000, -136.0552959530000123 ) ) ;
#1894=LINE ( 'NONE', #110, #16673 ) ;
#1897=VECTOR ( 'NONE', #16751, 1000.000000000000000 ) ;
#1906=EDGE_CURVE ( 'NONE', #3707, #18017, #5366, .T. ) ;
#1908=LINE ( 'NONE', #21656, #19722 ) ;
#1918=ORIENTED_EDGE ( 'NONE', *, *, #15768, .T. ) ;
#1919=CARTESIAN_POINT ( 'NONE',  ( -15.00000000000000000, -41.50000000000000000, -136.0552959530000123 ) ) ;
#1923=ADVANCED_FACE ( 'NONE', ( #14535 ), #18215, .F. ) ;
#1929=CIRCLE ( 'NONE', #21679, 1.500000000000001332 ) ;
#1930=ORIENTED_EDGE ( 'NONE', *, *, #5461, .T. ) ;
#1935=CARTESIAN_POINT ( 'NONE',  ( -13.50000000000000000, -43.00000000000000000, -136.0552959530000123 ) ) ;
#1937=ADVANCED_FACE ( 'NONE', ( #21437 ), #21798, .F. ) ;
#1939=LINE ( 'NONE', #12738, #2614 ) ;
#1942=AXIS2_PLACEMENT_3D ( 'NONE', #21792, #14397, #18087 ) ;
#1949=CARTESIAN_POINT ( 'NONE',  ( 3.611688725869999975E-11, 33.50000000000000000, -136.0552959530000123 ) ) ;
#1954=CARTESIAN_POINT ( 'NONE',  ( 9.479581287912614229, -35.03079462197541716, -136.0552959530214139 ) ) ;
#1959=LINE ( 'NONE', #274, #17162 ) ;
#1964=ORIENTED_EDGE ( 'NONE', *, *, #14914, .F. ) ;
#1972=CARTESIAN_POINT ( 'NONE',  ( -13.86630785130000021, 50.50000000000000000, -137.0552959530000123 ) ) ;
#1980=ORIENTED_EDGE ( 'NONE', *, *, #3260, .F. ) ;
#1982=EDGE_CURVE ( 'NONE', #3707, #10668, #19532, .T. ) ;
#1994=CARTESIAN_POINT ( 'NONE',  ( 22.89800326577455181, 33.50000000000002132, -136.0552959530517683 ) ) ;
#1995=EDGE_CURVE ( 'NONE', #8661, #7495, #22169, .T. ) ;
#1997=DIRECTION ( 'NONE',  ( 0.7071067811865469066, -0.7071067811865481278, -1.591319668629387474E-12 ) ) ;
#1999=CARTESIAN_POINT ( 'NONE',  ( 6.500000000040000003, 13.00000000000000000, -136.0552959530000123 ) ) ;
#2000=VERTEX_POINT ( 'NONE', #20000 ) ;
#2008=DIRECTION ( 'NONE',  ( 1.000000000000000000, 0.000000000000000000, -2.273736754470000126E-12 ) ) ;
#2009=ORIENTED_EDGE ( 'NONE', *, *, #3205, .F. ) ;
#2022=LINE ( 'NONE', #3228, #4549 ) ;
#2025=VECTOR ( 'NONE', #8459, 1000.000000000000000 ) ;
#2035=LINE ( 'NONE', #9364, #6058 ) ;
#2037=CARTESIAN_POINT ( 'NONE',  ( 31.50000000000000000, -33.03620104880000241, -136.5552959530000123 ) ) ;
#2057=EDGE_LOOP ( 'NONE', ( #5213, #12382, #8175, #20593 ) ) ;
#2068=EDGE_CURVE ( 'NONE', #15863, #16606, #9880, .T. ) ;
#2079=DIRECTION ( 'NONE',  ( 2.257749542879999954E-12, 0.000000000000000000, 1.000000000000000000 ) ) ;
#2084=CARTESIAN_POINT ( 'NONE',  ( 23.00000000000000000, 25.50000000000000000, -137.0552959530000123 ) ) ;
#2089=CARTESIAN_POINT ( 'NONE',  ( 3.298869075822184804, -4.420228454352442604, -136.0552959530074588 ) ) ;
#2096=FACE_OUTER_BOUND ( 'NONE', #10710, .T. ) ;
#2098=CARTESIAN_POINT ( 'NONE',  ( 25.42371301062762257, 37.28076054105333270, -136.0552959530573673 ) ) ;
#2101=LINE ( 'NONE', #14937, #8664 ) ;
#2120=VERTEX_POINT ( 'NONE', #11055 ) ;
#2139=ORIENTED_EDGE ( 'NONE', *, *, #3260, .T. ) ;
#2140=DIRECTION ( 'NONE',  ( 2.255973186040000320E-12, 0.000000000000000000, 1.000000000000000000 ) ) ;
#2141=ADVANCED_FACE ( 'NONE', ( #9615 ), #13193, .F. ) ;
#2160=DIRECTION ( 'NONE',  ( 2.257144641397284947E-12, -2.714590281723094849E-24, 1.000000000000000000 ) ) ;
#2184=CARTESIAN_POINT ( 'NONE',  ( -13.86630785130000021, -51.00000000000000000, -137.0552959530000123 ) ) ;
#2196=CARTESIAN_POINT ( 'NONE',  ( 3.611688725869999975E-11, 25.50000000000000000, -136.0552959530000123 ) ) ;
#2200=DIRECTION ( 'NONE',  ( -1.000000000000000000, 5.094701932209999624E-24, 0.000000000000000000 ) ) ;
#2203=EDGE_LOOP ( 'NONE', ( #7447, #5726, #22489, #13678 ) ) ;
#2217=DIRECTION ( 'NONE',  ( -1.000000000000000000, 5.094701932209999624E-24, 0.000000000000000000 ) ) ;
#2233=EDGE_LOOP ( 'NONE', ( #616, #16482, #10341, #10938 ) ) ;
#2241=CARTESIAN_POINT ( 'NONE',  ( 13.13369214870000157, 51.00000000000000000, -136.0552959530000123 ) ) ;
#2248=VECTOR ( 'NONE', #22620, 1000.000000000000000 ) ;
#2255=CARTESIAN_POINT ( 'NONE',  ( -7.499999999959999997, 45.50000000000000000, -136.0552959530000123 ) ) ;
#2257=EDGE_CURVE ( 'NONE', #6729, #16039, #20814, .T. ) ;
#2265=LINE ( 'NONE', #7714, #17477 ) ;
#2271=VERTEX_POINT ( 'NONE', #11746 ) ;
#2277=VERTEX_POINT ( 'NONE', #13542 ) ;
#2283=EDGE_CURVE ( 'NONE', #2271, #4317, #10201, .T. ) ;
#2286=ADVANCED_FACE ( 'NONE', ( #22597 ), #4744, .F. ) ;
#2295=CARTESIAN_POINT ( 'NONE',  ( 32.50000000000000000, 20.96379895120000114, -137.0552959530000123 ) ) ;
#2298=ORIENTED_EDGE ( 'NONE', *, *, #620, .T. ) ;
#2305=EDGE_CURVE ( 'NONE', #10668, #11605, #4633, .T. ) ;
#2309=LINE ( 'NONE', #7980, #13067 ) ;
#2310=AXIS2_PLACEMENT_3D ( 'NONE', #785, #6000, #16948 ) ;
#2334=FACE_OUTER_BOUND ( 'NONE', #22804, .T. ) ;
#2343=CARTESIAN_POINT ( 'NONE',  ( 14.00000000000000000, 20.50000000000000000, -136.0552959530000123 ) ) ;
#2360=VERTEX_POINT ( 'NONE', #7431 ) ;
#2361=DIRECTION ( 'NONE',  ( -0.6459422414661292189, 0.7633862853691524286, 1.457985068980292769E-12 ) ) ;
#2377=FACE_OUTER_BOUND ( 'NONE', #6841, .T. ) ;
#2408=CARTESIAN_POINT ( 'NONE',  ( 5.257430384941513601, -2.190056847782472005, -136.0552959530118642 ) ) ;
#2414=DIRECTION ( 'NONE',  ( 1.000000000000000000, 0.000000000000000000, -2.257453483404485639E-12 ) ) ;
#2421=DIRECTION ( 'NONE',  ( -1.000000000000000000, 0.000000000000000000, 2.273736754430000208E-12 ) ) ;
#2424=CARTESIAN_POINT ( 'NONE',  ( -15.00000000000000000, -41.50000000000000000, -137.0552959530000123 ) ) ;
#2430=ADVANCED_FACE ( 'NONE', ( #2096 ), #20296, .F. ) ;
#2440=EDGE_CURVE ( 'NONE', #7436, #4448, #592, .T. ) ;
#2454=VERTEX_POINT ( 'NONE', #16481 ) ;
#2461=EDGE_CURVE ( 'NONE', #5202, #15683, #6236, .T. ) ;
#2462=CARTESIAN_POINT ( 'NONE',  ( 32.00000000010000178, -33.03620104880000241, -136.0552959530000123 ) ) ;
#2469=ORIENTED_EDGE ( 'NONE', *, *, #18997, .F. ) ;
#2471=EDGE_LOOP ( 'NONE', ( #2009, #23532, #9432, #9647 ) ) ;
#2473=ORIENTED_EDGE ( 'NONE', *, *, #19713, .T. ) ;
#2474=ORIENTED_EDGE ( 'NONE', *, *, #19892, .T. ) ;
#2487=ORIENTED_EDGE ( 'NONE', *, *, #4265, .T. ) ;
#2503=CARTESIAN_POINT ( 'NONE',  ( 23.50000000000000000, -20.50000000000000000, -136.0552959530000123 ) ) ;
#2505=CARTESIAN_POINT ( 'NONE',  ( 6.750000000030000002, -44.75000000000000000, -136.0552959530000123 ) ) ;
#2512=CARTESIAN_POINT ( 'NONE',  ( -1.898424454282724216, 45.72687021304442112, -136.0552959529957207 ) ) ;
#2519=CARTESIAN_POINT ( 'NONE',  ( 3.611688725869999975E-11, 25.50000000000000000, -136.0552959530000123 ) ) ;
#2520=ORIENTED_EDGE ( 'NONE', *, *, #19556, .F. ) ;
#2521=DIRECTION ( 'NONE',  ( -2.257144641399999941E-12, 8.049635416090000264E-35, -1.000000000000000000 ) ) ;
#2526=LINE ( 'NONE', #9748, #2248 ) ;
#2528=CARTESIAN_POINT ( 'NONE',  ( -4.499999999959999109, 34.00000000000000000, -136.0552959530000123 ) ) ;
#2536=PLANE ( 'NONE',  #5799 ) ;
#2556=CARTESIAN_POINT ( 'NONE',  ( 13.13369214870000157, -2.273736754430000208E-12, -136.0552959530000123 ) ) ;
#2561=DIRECTION ( 'NONE',  ( -1.000000000000000000, 0.000000000000000000, 2.257120985840000117E-12 ) ) ;
#2573=EDGE_LOOP ( 'NONE', ( #11204, #11882, #8757, #13422 ) ) ;
#2575=ORIENTED_EDGE ( 'NONE', *, *, #11511, .T. ) ;
#2579=DIRECTION ( 'NONE',  ( 0.000000000000000000, -1.000000000000000000, 0.000000000000000000 ) ) ;
#2582=VECTOR ( 'NONE', #19877, 1000.000000000000000 ) ;
#2597=AXIS2_PLACEMENT_3D ( 'NONE', #20775, #15306, #8139 ) ;
#2598=PLANE ( 'NONE',  #20129 ) ;
#2602=VERTEX_POINT ( 'NONE', #4338 ) ;
#2609=PLANE ( 'NONE',  #8684 ) ;
#2614=VECTOR ( 'NONE', #12850, 1000.000000000000000 ) ;
#2646=CARTESIAN_POINT ( 'NONE',  ( -9.999999999959999997, 42.50000000000000000, -136.0552959530000123 ) ) ;
#2650=LINE ( 'NONE', #2184, #14973 ) ;
#2655=DIRECTION ( 'NONE',  ( 0.000000000000000000, 1.000000000000000000, 0.000000000000000000 ) ) ;
#2656=ORIENTED_EDGE ( 'NONE', *, *, #4863, .T. ) ;
#2657=VECTOR ( 'NONE', #14851, 1000.000000000000227 ) ;
#2675=VECTOR ( 'NONE', #17204, 1000.000000000000000 ) ;
#2684=VERTEX_POINT ( 'NONE', #12289 ) ;
#2685=CARTESIAN_POINT ( 'NONE',  ( -4.499999999969999109, 34.00000000000000000, -137.0552959530000123 ) ) ;
#2686=EDGE_CURVE ( 'NONE', #16611, #20903, #6473, .T. ) ;
#2704=CARTESIAN_POINT ( 'NONE',  ( 6.007013984479645963, 28.00000000000003197, -136.0552959530135979 ) ) ;
#2717=EDGE_CURVE ( 'NONE', #19898, #18293, #13851, .T. ) ;
#2719=DIRECTION ( 'NONE',  ( -1.000000000000000000, 5.094701932209999624E-24, 2.257144641399999941E-12 ) ) ;
#2723=ADVANCED_FACE ( 'NONE', ( #1138 ), #8368, .F. ) ;
#2738=CARTESIAN_POINT ( 'NONE',  ( -3.499999999959999997, 34.00000000000000000, -136.0552959530000123 ) ) ;
#2752=B_SPLINE_CURVE_WITH_KNOTS ( 'NONE', 3,
 ( #5830, #9622, #495, #8078, #18799, #11177, #20596, #18915, #20705, #17131 ),
 .UNSPECIFIED., .F., .F.,
 ( 4, 2, 2, 2, 4 ),
 ( 0.000000000000000000, 0.2499999999999985012, 0.4999999999999990008, 0.7499999999999994449, 1.000000000000000000 ),
 .UNSPECIFIED. ) ;
#2757=FACE_OUTER_BOUND ( 'NONE', #2887, .T. ) ;
#2759=AXIS2_PLACEMENT_3D ( 'NONE', #1416, #14369, #1306 ) ;
#2764=LINE ( 'NONE', #19166, #18192 ) ;
#2791=ORIENTED_EDGE ( 'NONE', *, *, #2440, .F. ) ;
#2795=EDGE_LOOP ( 'NONE', ( #15530, #15621, #18074, #13138 ) ) ;
#2802=FACE_BOUND ( 'NONE', #7788, .T. ) ;
#2803=FACE_OUTER_BOUND ( 'NONE', #950, .T. ) ;
#2805=DIRECTION ( 'NONE',  ( 1.000000000000000000, 0.000000000000000000, -2.257453483404485235E-12 ) ) ;
#2815=ORIENTED_EDGE ( 'NONE', *, *, #21780, .F. ) ;
#2849=DIRECTION ( 'NONE',  ( 2.256861364460000137E-12, 0.000000000000000000, 1.000000000000000000 ) ) ;
#2853=EDGE_CURVE ( 'NONE', #19866, #13875, #5393, .T. ) ;
#2854=DIRECTION ( 'NONE',  ( -1.000000000000000000, 0.000000000000000000, 2.257120985840000117E-12 ) ) ;
#2859=EDGE_CURVE ( 'NONE', #5950, #5202, #2650, .T. ) ;
#2860=EDGE_CURVE ( 'NONE', #17363, #12377, #2309, .T. ) ;
#2863=FACE_OUTER_BOUND ( 'NONE', #12833, .T. ) ;
#2881=DIRECTION ( 'NONE',  ( 1.000000000000000000, 0.000000000000000000, -2.262368070660000099E-12 ) ) ;
#2885=EDGE_CURVE ( 'NONE', #546, #14999, #14216, .T. ) ;
#2887=EDGE_LOOP ( 'NONE', ( #19953, #13891, #13269, #16498 ) ) ;
#2889=DIRECTION ( 'NONE',  ( 5.094701932209999624E-24, 1.000000000000000000, 0.000000000000000000 ) ) ;
#2892=AXIS2_PLACEMENT_3D ( 'NONE', #9069, #7528, #21838 ) ;
#2905=ORIENTED_EDGE ( 'NONE', *, *, #3505, .T. ) ;
#2923=CARTESIAN_POINT ( 'NONE',  ( -32.50000000000000000, 21.50000000000000000, -137.0552959530000123 ) ) ;
#2931=ORIENTED_EDGE ( 'NONE', *, *, #4863, .F. ) ;
#2932=CARTESIAN_POINT ( 'NONE',  ( 1.544832289376347534, 26.15117705467465115, -136.0552959530034798 ) ) ;
#2935=VERTEX_POINT ( 'NONE', #22164 ) ;
#2961=EDGE_LOOP ( 'NONE', ( #20948, #1183, #3454, #23267 ) ) ;
#2987=CARTESIAN_POINT ( 'NONE',  ( -32.50000000000000000, 21.50000000000000000, -136.0552959530000123 ) ) ;
#2988=VECTOR ( 'NONE', #6917, 1000.000000000000000 ) ;
#2997=DIRECTION ( 'NONE',  ( -1.000000000000000000, 5.094701932209999624E-24, 0.000000000000000000 ) ) ;
#3002=LINE ( 'NONE', #6438, #21364 ) ;
#3015=ORIENTED_EDGE ( 'NONE', *, *, #10411, .T. ) ;
#3016=AXIS2_PLACEMENT_3D ( 'NONE', #9727, #4167, #17003 ) ;
#3021=CARTESIAN_POINT ( 'NONE',  ( -12.50000000000000000, 45.50000000000000000, -137.0552959530000123 ) ) ;
#3030=AXIS2_PLACEMENT_3D ( 'NONE', #3237, #21215, #10587 ) ;
#3038=CARTESIAN_POINT ( 'NONE',  ( 32.50000000000000000, 20.96379895120000114, -136.0552959530000123 ) ) ;
#3051=VECTOR ( 'NONE', #8892, 1000.000000000000000 ) ;
#3061=DIRECTION ( 'NONE',  ( -1.000000000000000000, 5.094701932209999624E-24, 2.257144641399999941E-12 ) ) ;
#3064=ORIENTED_EDGE ( 'NONE', *, *, #19556, .T. ) ;
#3071=ORIENTED_EDGE ( 'NONE', *, *, #13452, .T. ) ;
#3072=CARTESIAN_POINT ( 'NONE',  ( 3.611688725869999975E-11, 48.50000000000000000, -136.0552959530000123 ) ) ;
#3076=EDGE_CURVE ( 'NONE', #12377, #11046, #9755, .T. ) ;
#3085=FACE_OUTER_BOUND ( 'NONE', #9259, .T. ) ;
#3098=VECTOR ( 'NONE', #14342, 1000.000000000000000 ) ;
#3100=ORIENTED_EDGE ( 'NONE', *, *, #5461, .F. ) ;
#3126=DIRECTION ( 'NONE',  ( 2.257157423930000049E-12, 0.000000000000000000, 1.000000000000000000 ) ) ;
#3128=EDGE_CURVE ( 'NONE', #11242, #23163, #18023, .T. ) ;
#3146=ORIENTED_EDGE ( 'NONE', *, *, #21481, .T. ) ;
#3151=VECTOR ( 'NONE', #15317, 1000.000000000000000 ) ;
#3198=EDGE_LOOP ( 'NONE', ( #4763, #9828, #8564, #21855 ) ) ;
#3201=EDGE_CURVE ( 'NONE', #20903, #16332, #17273, .T. ) ;
#3205=EDGE_CURVE ( 'NONE', #16693, #21987, #19293, .T. ) ;
#3211=AXIS2_PLACEMENT_3D ( 'NONE', #15260, #22396, #22517 ) ;
#3214=CARTESIAN_POINT ( 'NONE',  ( -9.999999999959999997, 25.50000000000000000, -136.0552959530000123 ) ) ;
#3220=DIRECTION ( 'NONE',  ( 1.000000000000000000, -5.094701932209999624E-24, 0.000000000000000000 ) ) ;
#3228=CARTESIAN_POINT ( 'NONE',  ( -1.499999999969999998, 44.50000000000000000, -136.5552959530000123 ) ) ;
#3234=EDGE_CURVE ( 'NONE', #6536, #11683, #23450, .T. ) ;
#3237=CARTESIAN_POINT ( 'NONE',  ( -13.86630785130000021, 51.00000000000000000, -136.0552959530000123 ) ) ;
#3243=VECTOR ( 'NONE', #11888, 1000.000000000000000 ) ;
#3247=CARTESIAN_POINT ( 'NONE',  ( 6.500000000040000003, 20.50000000000000000, -136.0552959530000123 ) ) ;
#3248=CARTESIAN_POINT ( 'NONE',  ( 6.148946002053968130, -30.79517854816079137, -136.0552959530138821 ) ) ;
#3260=EDGE_CURVE ( 'NONE', #15679, #7495, #16718, .T. ) ;
#3265=CARTESIAN_POINT ( 'NONE',  ( 7.014880255720557400, -46.74993274156790335, -136.0552959530158716 ) ) ;
#3270=LINE ( 'NONE', #21130, #8236 ) ;
#3274=PLANE ( 'NONE',  #9800 ) ;
#3282=ORIENTED_EDGE ( 'NONE', *, *, #9812, .F. ) ;
#3289=FACE_OUTER_BOUND ( 'NONE', #2203, .T. ) ;
#3290=ORIENTED_EDGE ( 'NONE', *, *, #15799, .F. ) ;
#3291=FACE_OUTER_BOUND ( 'NONE', #21899, .T. ) ;
#3310=CARTESIAN_POINT ( 'NONE',  ( -4.020716686263415163, 46.44926652720589999, -136.0552959529909174 ) ) ;
#3322=AXIS2_PLACEMENT_3D ( 'NONE', #17018, #2521, #2414 ) ;
#3324=CARTESIAN_POINT ( 'NONE',  ( 32.50000000000000000, -2.273736754430000208E-12, -136.0552959530000123 ) ) ;
#3337=CARTESIAN_POINT ( 'NONE',  ( 8.750000000030000891, -36.98606797749999942, -136.0552959530000123 ) ) ;
#3339=DIRECTION ( 'NONE',  ( -0.7071067811865473507, 0.7071067811865476838, 1.591319668629389897E-12 ) ) ;
#3341=VECTOR ( 'NONE', #10644, 1000.000000000000000 ) ;
#3347=LINE ( 'NONE', #22878, #10181 ) ;
#3353=FACE_OUTER_BOUND ( 'NONE', #2471, .T. ) ;
#3355=CARTESIAN_POINT ( 'NONE',  ( -7.499999999959999997, 42.50000000000000000, -136.0552959530000123 ) ) ;
#3360=DIRECTION ( 'NONE',  ( 2.257144641399999941E-12, -8.049635380228619169E-35, 1.000000000000000000 ) ) ;
#3362=EDGE_CURVE ( 'NONE', #1359, #20086, #21685, .T. ) ;
#3378=VECTOR ( 'NONE', #1850, 1000.000000000000000 ) ;
#3385=CARTESIAN_POINT ( 'NONE',  ( -1.552054646623368228, 43.97650423128144581, -136.0552959530043893 ) ) ;
#3398=ORIENTED_EDGE ( 'NONE', *, *, #15067, .T. ) ;
#3399=CARTESIAN_POINT ( 'NONE',  ( 32.00000000000000000, -21.03620104879999886, -136.0552959530000123 ) ) ;
#3403=CARTESIAN_POINT ( 'NONE',  ( 31.50000000000000000, -2.273736754430000208E-12, -136.0552959530000123 ) ) ;
#3405=FACE_BOUND ( 'NONE', #14693, .T. ) ;
#3408=ORIENTED_EDGE ( 'NONE', *, *, #18526, .T. ) ;
#3412=ADVANCED_FACE ( 'NONE', ( #16199 ), #5243, .F. ) ;
#3416=EDGE_CURVE ( 'NONE', #416, #1359, #17986, .T. ) ;
#3420=ADVANCED_FACE ( 'NONE', ( #18560 ), #11406, .F. ) ;
#3423=CARTESIAN_POINT ( 'NONE',  ( -7.499999999969999109, 25.50000000000000000, -137.0552959530000123 ) ) ;
#3433=ORIENTED_EDGE ( 'NONE', *, *, #8802, .T. ) ;
#3454=ORIENTED_EDGE ( 'NONE', *, *, #8434, .F. ) ;
#3461=ORIENTED_EDGE ( 'NONE', *, *, #20108, .F. ) ;
#3462=DIRECTION ( 'NONE',  ( -2.257144641399999941E-12, 0.000000000000000000, -1.000000000000000000 ) ) ;
#3469=ORIENTED_EDGE ( 'NONE', *, *, #6101, .T. ) ;
#3475=CARTESIAN_POINT ( 'NONE',  ( 32.00000000000000000, 32.96379895120000469, -136.0552959530000123 ) ) ;
#3486=AXIS2_PLACEMENT_3D ( 'NONE', #3337, #8671, #15955 ) ;
#3488=CARTESIAN_POINT ( 'NONE',  ( 4.798892695445801770, -31.45134726954360005, -136.0552959530108694 ) ) ;
#3498=FACE_OUTER_BOUND ( 'NONE', #4609, .T. ) ;
#3504=DIRECTION ( 'NONE',  ( 2.257144641397284947E-12, 2.714724913984255017E-24, 1.000000000000000000 ) ) ;
#3505=EDGE_CURVE ( 'NONE', #7477, #14486, #11858, .T. ) ;
#3525=ORIENTED_EDGE ( 'NONE', *, *, #3128, .F. ) ;
#3533=CARTESIAN_POINT ( 'NONE',  ( 4.500000000009999113, -5.000000000000000000, -137.0552959530000123 ) ) ;
#3547=ORIENTED_EDGE ( 'NONE', *, *, #4558, .F. ) ;
#3551=CARTESIAN_POINT ( 'NONE',  ( -4.726870213007021704, 46.10157554568331761, -136.0552959529892973 ) ) ;
#3556=VERTEX_POINT ( 'NONE', #15813 ) ;
#3564=DIRECTION ( 'NONE',  ( 1.000000000000000000, 0.000000000000000000, -2.254788948169999945E-12 ) ) ;
#3578=LINE ( 'NONE', #9021, #11073 ) ;
#3583=DIRECTION ( 'NONE',  ( 5.094701932209999624E-24, 1.000000000000000000, 0.000000000000000000 ) ) ;
#3593=CARTESIAN_POINT ( 'NONE',  ( 8.750000000030000891, -44.75000000000000000, -137.0552959530000123 ) ) ;
#3596=B_SPLINE_CURVE_WITH_KNOTS ( 'NONE', 3,
 ( #5948, #13202, #20475, #18692, #7840, #2512, #20950, #1321, #15704, #4873 ),
 .UNSPECIFIED., .F., .F.,
 ( 4, 2, 2, 2, 4 ),
 ( 0.000000000000000000, 0.2500000000000000000, 0.5000000000000000000, 0.7500000000000000000, 1.000000000000000000 ),
 .UNSPECIFIED. ) ;
#3628=CARTESIAN_POINT ( 'NONE',  ( 20.50000000000000000, 22.50000000000000000, -137.0552959530000123 ) ) ;
#3629=LINE ( 'NONE', #3864, #19188 ) ;
#3640=CIRCLE ( 'NONE', #4773, 2.999999999999999112 ) ;
#3642=ORIENTED_EDGE ( 'NONE', *, *, #11610, .F. ) ;
#3647=EDGE_LOOP ( 'NONE', ( #3064, #16595, #12746, #18365 ) ) ;
#3651=LINE ( 'NONE', #5657, #1368 ) ;
#3656=CARTESIAN_POINT ( 'NONE',  ( 32.00000000000000000, -33.03620104880000241, -137.0552959530000123 ) ) ;
#3660=ORIENTED_EDGE ( 'NONE', *, *, #13176, .T. ) ;
#3669=EDGE_LOOP ( 'NONE', ( #3751, #13052, #5832, #1710 ) ) ;
#3672=CARTESIAN_POINT ( 'NONE',  ( 4.500000000009999113, -2.000000000000000000, -136.0552959530000123 ) ) ;
#3683=CARTESIAN_POINT ( 'NONE',  ( 32.50000000000000000, -33.03620104880000241, -137.0552959530000123 ) ) ;
#3688=CARTESIAN_POINT ( 'NONE',  ( 0.8488229453839356564, 15.54483228932016026, -136.0552959530018882 ) ) ;
#3699=CARTESIAN_POINT ( 'NONE',  ( 4.750000000030000002, -40.36803398869999882, -137.0552959530000123 ) ) ;
#3707=VERTEX_POINT ( 'NONE', #19623 ) ;
#3714=ORIENTED_EDGE ( 'NONE', *, *, #5932, .T. ) ;
#3727=CARTESIAN_POINT ( 'NONE',  ( -4.500067286917269982, 22.89748944254629848, -136.0552959529898658 ) ) ;
#3746=VERTEX_POINT ( 'NONE', #7244 ) ;
#3751=ORIENTED_EDGE ( 'NONE', *, *, #21172, .T. ) ;
#3757=VECTOR ( 'NONE', #19748, 1000.000000000000000 ) ;
#3760=CARTESIAN_POINT ( 'NONE',  ( -3.499999999959999997, 46.50000000000000000, -136.0552959530000123 ) ) ;
#3766=EDGE_CURVE ( 'NONE', #2602, #2360, #1929, .T. ) ;
#3770=DIRECTION ( 'NONE',  ( 7.105427352750000330E-15, -1.000000000000000000, -1.603797727410000024E-26 ) ) ;
#3775=ORIENTED_EDGE ( 'NONE', *, *, #16484, .T. ) ;
#3782=CARTESIAN_POINT ( 'NONE',  ( -3.765581077008664401, 46.50000000000002842, -136.0552959529915142 ) ) ;
#3791=LINE ( 'NONE', #219, #16054 ) ;
#3792=CARTESIAN_POINT ( 'NONE',  ( 13.13369214870000157, 51.50000000000000000, -137.0552959530000123 ) ) ;
#3795=AXIS2_PLACEMENT_3D ( 'NONE', #22433, #13384, #20652 ) ;
#3823=CARTESIAN_POINT ( 'NONE',  ( -13.53904098499752884, -43.39262182653893518, -136.0552959530033377 ) ) ;
#3836=VERTEX_POINT ( 'NONE', #8891 ) ;
#3841=FACE_OUTER_BOUND ( 'NONE', #20320, .T. ) ;
#3844=CARTESIAN_POINT ( 'NONE',  ( 17.49993271309341125, 22.89748944248912466, -136.0552959530394617 ) ) ;
#3847=DIRECTION ( 'NONE',  ( 2.256861364460000137E-12, 0.000000000000000000, 1.000000000000000000 ) ) ;
#3854=EDGE_CURVE ( 'NONE', #2360, #2602, #14067, .T. ) ;
#3856=CARTESIAN_POINT ( 'NONE',  ( -9.999999999969999109, 42.50000000000000000, -137.0552959530000123 ) ) ;
#3864=CARTESIAN_POINT ( 'NONE',  ( 1.133692148650000009, 50.50000000000000000, -136.5552959530000123 ) ) ;
#3865=LINE ( 'NONE', #7424, #16629 ) ;
#3867=ORIENTED_EDGE ( 'NONE', *, *, #14460, .T. ) ;
#3872=ORIENTED_EDGE ( 'NONE', *, *, #9924, .T. ) ;
#3882=CARTESIAN_POINT ( 'NONE',  ( 24.01497134763214802, 33.88109793996618890, -136.0552959530542125 ) ) ;
#3891=CARTESIAN_POINT ( 'NONE',  ( 8.750000000030000891, -39.98606797749999942, -136.5552959530000123 ) ) ;
#3901=VERTEX_POINT ( 'NONE', #3792 ) ;
#3903=ORIENTED_EDGE ( 'NONE', *, *, #12855, .T. ) ;
#3917=CARTESIAN_POINT ( 'NONE',  ( 32.50000000000000000, -21.03620104879999886, -136.0552959530000123 ) ) ;
#3918=CARTESIAN_POINT ( 'NONE',  ( 13.13369214870000157, -51.00000000000000000, -136.0552959530000123 ) ) ;
#3930=CARTESIAN_POINT ( 'NONE',  ( 31.50000000000000000, 20.96379895120000114, -137.0552959530000123 ) ) ;
#3944=ORIENTED_EDGE ( 'NONE', *, *, #15067, .F. ) ;
#3962=CARTESIAN_POINT ( 'NONE',  ( 13.13369214870000157, 51.50000000000000000, -136.5552959530000123 ) ) ;
#3973=LINE ( 'NONE', #9418, #11219 ) ;
#3977=DIRECTION ( 'NONE',  ( 0.000000000000000000, 1.000000000000000000, 0.000000000000000000 ) ) ;
#3986=EDGE_CURVE ( 'NONE', #18032, #5950, #9699, .T. ) ;
#3987=CARTESIAN_POINT ( 'NONE',  ( 7.480639893073429469, 27.95196862336259258, -136.0552959530169232 ) ) ;
#3990=CARTESIAN_POINT ( 'NONE',  ( -13.86630785130000021, 50.50000000000000000, -136.0552959530000123 ) ) ;
#4000=EDGE_LOOP ( 'NONE', ( #5638, #20070, #4641, #8074 ) ) ;
#4024=CARTESIAN_POINT ( 'NONE',  ( 7.750000000030000002, -37.98606797749999942, -137.0552959530000123 ) ) ;
#4025=ORIENTED_EDGE ( 'NONE', *, *, #6716, .T. ) ;
#4027=AXIS2_PLACEMENT_3D ( 'NONE', #22435, #8134, #6245 ) ;
#4035=EDGE_LOOP ( 'NONE', ( #11037, #9057, #10491, #13868 ) ) ;
#4036=CARTESIAN_POINT ( 'NONE',  ( -0.9999999999639999082, 20.50000000000000000, -136.0552959530000123 ) ) ;
#4037=CARTESIAN_POINT ( 'NONE',  ( 8.750000000030000891, -44.75000000000000000, -136.0552959530000123 ) ) ;
#4048=ORIENTED_EDGE ( 'NONE', *, *, #12119, .F. ) ;
#4051=CARTESIAN_POINT ( 'NONE',  ( -5.246332635998737892, 43.48990303079973074, -136.0552959529881889 ) ) ;
#4057=ORIENTED_EDGE ( 'NONE', *, *, #3362, .F. ) ;
#4073=CARTESIAN_POINT ( 'NONE',  ( 4.750000000030000002, -2.273736754430000208E-12, -136.0552959530000123 ) ) ;
#4091=CARTESIAN_POINT ( 'NONE',  ( -13.86630785130000021, 51.00000000000000000, -137.0552959530000123 ) ) ;
#4112=LINE ( 'NONE', #14835, #9155 ) ;
#4136=ADVANCED_FACE ( 'NONE', ( #3289 ), #8621, .T. ) ;
#4139=AXIS2_PLACEMENT_3D ( 'NONE', #2505, #20585, #20354 ) ;
#4144=CARTESIAN_POINT ( 'NONE',  ( 3.038243779794036037, -3.109320143290841276, -136.0552959530068620 ) ) ;
#4161=ORIENTED_EDGE ( 'NONE', *, *, #506, .T. ) ;
#4162=EDGE_CURVE ( 'NONE', #6084, #13875, #23160, .T. ) ;
#4166=AXIS2_PLACEMENT_3D ( 'NONE', #16030, #1530, #4845 ) ;
#4167=DIRECTION ( 'NONE',  ( -2.257144641399999941E-12, 8.049635416090000264E-35, -1.000000000000000000 ) ) ;
#4170=VERTEX_POINT ( 'NONE', #5185 ) ;
#4191=CARTESIAN_POINT ( 'NONE',  ( 12.88080765325204879, 38.01462304342913967, -136.0552959530290593 ) ) ;
#4196=CARTESIAN_POINT ( 'NONE',  ( -7.499999999969999109, 42.50000000000000000, -136.5552959530000123 ) ) ;
#4199=AXIS2_PLACEMENT_3D ( 'NONE', #21594, #10738, #18018 ) ;
#4210=DIRECTION ( 'NONE',  ( -1.000000000000000000, 5.094701932209999624E-24, 2.257144641399999941E-12 ) ) ;
#4214=VECTOR ( 'NONE', #2079, 1000.000000000000000 ) ;
#4226=EDGE_CURVE ( 'NONE', #15863, #2602, #17801, .T. ) ;
#4227=CARTESIAN_POINT ( 'NONE',  ( 25.11896946145980891, 38.01480899506201183, -136.0552959530567421 ) ) ;
#4234=FACE_BOUND ( 'NONE', #6141, .T. ) ;
#4247=ORIENTED_EDGE ( 'NONE', *, *, #14914, .T. ) ;
#4252=CARTESIAN_POINT ( 'NONE',  ( -13.86630785130000021, -50.50000000000000000, -136.5552959530000123 ) ) ;
#4264=DIRECTION ( 'NONE',  ( 1.000000000000000000, 0.000000000000000000, -2.257157423930000049E-12 ) ) ;
#4265=EDGE_CURVE ( 'NONE', #12804, #15239, #1521, .T. ) ;
#4269=CARTESIAN_POINT ( 'NONE',  ( 31.50000000000000000, -0.03620104880649999829, -136.0552959530000123 ) ) ;
#4272=DIRECTION ( 'NONE',  ( 1.000000000000000000, 0.000000000000000000, -2.257453483404485639E-12 ) ) ;
#4274=EDGE_CURVE ( 'NONE', #15302, #18787, #11703, .T. ) ;
#4286=VERTEX_POINT ( 'NONE', #4426 ) ;
#4289=ADVANCED_FACE ( 'NONE', ( #17157 ), #21858, .T. ) ;
#4301=FACE_OUTER_BOUND ( 'NONE', #5759, .T. ) ;
#4304=EDGE_CURVE ( 'NONE', #12120, #8637, #2101, .T. ) ;
#4312=ADVANCED_FACE ( 'NONE', ( #7668 ), #16594, .F. ) ;
#4317=VERTEX_POINT ( 'NONE', #86 ) ;
#4319=CARTESIAN_POINT ( 'NONE',  ( -15.00000000000000000, -43.00000000000000000, -137.0552959530000123 ) ) ;
#4326=CARTESIAN_POINT ( 'NONE',  ( 13.13369214870000157, 50.50000000000000000, -136.5552959530000123 ) ) ;
#4331=VECTOR ( 'NONE', #17475, 1000.000000000000000 ) ;
#4335=ORIENTED_EDGE ( 'NONE', *, *, #9812, .T. ) ;
#4338=CARTESIAN_POINT ( 'NONE',  ( 22.00000000000000000, -20.50000000000000000, -137.0552959530000123 ) ) ;
#4356=VERTEX_POINT ( 'NONE', #3760 ) ;
#4358=ORIENTED_EDGE ( 'NONE', *, *, #19128, .T. ) ;
#4361=ORIENTED_EDGE ( 'NONE', *, *, #9154, .F. ) ;
#4363=DIRECTION ( 'NONE',  ( 2.257749542879999954E-12, 0.000000000000000000, 1.000000000000000000 ) ) ;
#4374=EDGE_CURVE ( 'NONE', #10468, #3556, #18284, .T. ) ;
#4400=EDGE_CURVE ( 'NONE', #13712, #16611, #7435, .T. ) ;
#4411=DIRECTION ( 'NONE',  ( 1.000000000000000000, 0.000000000000000000, -2.257120985840000117E-12 ) ) ;
#4426=CARTESIAN_POINT ( 'NONE',  ( 13.13369214870000157, -50.50000000000000000, -137.0552959530000123 ) ) ;
#4436=LINE ( 'NONE', #7762, #23034 ) ;
#4439=FACE_OUTER_BOUND ( 'NONE', #2057, .T. ) ;
#4445=VECTOR ( 'NONE', #17965, 1000.000000000000000 ) ;
#4448=VERTEX_POINT ( 'NONE', #19422 ) ;
#4454=CARTESIAN_POINT ( 'NONE',  ( -4.499999999969999109, 40.00000000000000000, -136.5552959530000123 ) ) ;
#4458=EDGE_CURVE ( 'NONE', #20106, #19866, #3347, .T. ) ;
#4465=PLANE ( 'NONE',  #16974 ) ;
#4469=ORIENTED_EDGE ( 'NONE', *, *, #9466, .F. ) ;
#4487=EDGE_CURVE ( 'NONE', #21201, #16725, #10358, .T. ) ;
#4496=CARTESIAN_POINT ( 'NONE',  ( 4.500000000009999113, -2.000000000000000000, -137.0552959530000123 ) ) ;
#4498=LINE ( 'NONE', #11738, #8710 ) ;
#4525=VECTOR ( 'NONE', #15066, 1000.000000000000000 ) ;
#4534=DIRECTION ( 'NONE',  ( 1.000000000000000000, 0.000000000000000000, -2.257453483404485639E-12 ) ) ;
#4535=ORIENTED_EDGE ( 'NONE', *, *, #7925, .T. ) ;
#4544=FACE_OUTER_BOUND ( 'NONE', #8746, .T. ) ;
#4549=VECTOR ( 'NONE', #15959, 1000.000000000000000 ) ;
#4552=CIRCLE ( 'NONE', #16347, 2.999999999999999112 ) ;
#4557=FACE_OUTER_BOUND ( 'NONE', #6240, .T. ) ;
#4558=EDGE_CURVE ( 'NONE', #15020, #3901, #1939, .T. ) ;
#4574=CARTESIAN_POINT ( 'NONE',  ( -2.499999999959999997, 40.00000000000000000, -136.0552959530000123 ) ) ;
#4585=CARTESIAN_POINT ( 'NONE',  ( -32.50000000000000000, 51.50000000000000000, -137.0552959530000123 ) ) ;
#4590=CARTESIAN_POINT ( 'NONE',  ( 0.000000000000000000, 0.000000000000000000, 0.000000000000000000 ) ) ;
#4596=CARTESIAN_POINT ( 'NONE',  ( 1.924079216191155073, 26.46241645103238582, -136.0552959530043609 ) ) ;
#4601=ORIENTED_EDGE ( 'NONE', *, *, #3362, .T. ) ;
#4609=EDGE_LOOP ( 'NONE', ( #17653, #22994, #13312, #11168 ) ) ;
#4610=LINE ( 'NONE', #21037, #15157 ) ;
#4618=DIRECTION ( 'NONE',  ( -2.257144641399999941E-12, 0.000000000000000000, -1.000000000000000000 ) ) ;
#4626=CARTESIAN_POINT ( 'NONE',  ( -2.499999999959999997, 37.00000000000000000, -136.0552959530000123 ) ) ;
#4633=LINE ( 'NONE', #20940, #4331 ) ;
#4635=DIRECTION ( 'NONE',  ( 2.257144641399999941E-12, -8.049635396172279677E-35, 1.000000000000000000 ) ) ;
#4637=VERTEX_POINT ( 'NONE', #3593 ) ;
#4641=ORIENTED_EDGE ( 'NONE', *, *, #8554, .F. ) ;
#4647=DIRECTION ( 'NONE',  ( 2.259525899719999991E-12, 0.000000000000000000, 1.000000000000000000 ) ) ;
#4649=CARTESIAN_POINT ( 'NONE',  ( 31.50000000000000000, -36.53620104879999531, -136.0552959530000123 ) ) ;
#4650=ORIENTED_EDGE ( 'NONE', *, *, #10411, .F. ) ;
#4661=CARTESIAN_POINT ( 'NONE',  ( 8.250000000030000891, -39.98606797749999942, -136.0552959530000123 ) ) ;
#4666=VERTEX_POINT ( 'NONE', #10940 ) ;
#4673=DIRECTION ( 'NONE',  ( 2.257144641397284947E-12, -2.714724913984255017E-24, 1.000000000000000000 ) ) ;
#4674=EDGE_CURVE ( 'NONE', #15679, #7623, #2752, .T. ) ;
#4678=CARTESIAN_POINT ( 'NONE',  ( 16.13369214859999801, 50.50000000000000000, -137.0552959530000123 ) ) ;
#4679=CARTESIAN_POINT ( 'NONE',  ( 8.750000000030000891, -37.98606797749999942, -137.0552959530000123 ) ) ;
#4688=CYLINDRICAL_SURFACE ( 'NONE', #12949, 1.500000000000001332 ) ;
#4694=DIRECTION ( 'NONE',  ( -2.257144641399999941E-12, 8.049635416090000264E-35, -1.000000000000000000 ) ) ;
#4714=ORIENTED_EDGE ( 'NONE', *, *, #17217, .F. ) ;
#4723=EDGE_LOOP ( 'NONE', ( #13185, #9735, #15541, #19053 ) ) ;
#4744=PLANE ( 'NONE',  #10393 ) ;
#4745=ORIENTED_EDGE ( 'NONE', *, *, #19694, .F. ) ;
#4746=DIRECTION ( 'NONE',  ( 1.000000000000000000, 0.000000000000000000, -2.257120985840000117E-12 ) ) ;
#4755=B_SPLINE_CURVE_WITH_KNOTS ( 'NONE', 3,
 ( #16119, #5161, #17778, #7185, #10281, #19461, #17553, #1270, #3265, #8493, #14097, #17905, #15763, #12407, #10391, #17665, #1374, #5058 ),
 .UNSPECIFIED., .F., .F.,
 ( 4, 2, 2, 2, 2, 2, 2, 2, 4 ),
 ( 0.000000000000000000, 0.1250000000000000000, 0.2500000000000000000, 0.3750000000000000000, 0.5000000000000000000, 0.6250000000000000000, 0.7500000000000000000, 0.8750000000000000000, 1.000000000000000000 ),
 .UNSPECIFIED. ) ;
#4759=DIRECTION ( 'NONE',  ( -0.7071067811865471286, 0.7071067811865477948, 1.595945597898661113E-12 ) ) ;
#4760=DIRECTION ( 'NONE',  ( 0.000000000000000000, 1.000000000000000000, 0.000000000000000000 ) ) ;
#4762=CARTESIAN_POINT ( 'NONE',  ( -9.999999999959999997, 48.50000000000000000, -136.0552959530000123 ) ) ;
#4763=ORIENTED_EDGE ( 'NONE', *, *, #2885, .F. ) ;
#4773=AXIS2_PLACEMENT_3D ( 'NONE', #12684, #92, #12915 ) ;
#4774=VERTEX_POINT ( 'NONE', #16895 ) ;
#4776=DIRECTION ( 'NONE',  ( 2.255973186040000320E-12, 0.000000000000000000, 1.000000000000000000 ) ) ;
#4780=ORIENTED_EDGE ( 'NONE', *, *, #18061, .T. ) ;
#4784=ORIENTED_EDGE ( 'NONE', *, *, #10976, .F. ) ;
#4786=EDGE_CURVE ( 'NONE', #4356, #16880, #3596, .T. ) ;
#4796=ORIENTED_EDGE ( 'NONE', *, *, #3201, .F. ) ;
#4825=VERTEX_POINT ( 'NONE', #19397 ) ;
#4827=EDGE_LOOP ( 'NONE', ( #52, #95, #4469, #11592 ) ) ;
#4828=PRESENTATION_STYLE_ASSIGNMENT (( #16008 ) ) ;
#4835=ORIENTED_EDGE ( 'NONE', *, *, #57, .F. ) ;
#4845=DIRECTION ( 'NONE',  ( 0.7071067811865474617, 0.7071067811865476838, -1.595020412044806951E-12 ) ) ;
#4853=DIRECTION ( 'NONE',  ( -1.000000000000000000, 0.000000000000000000, 2.257495777610000006E-12 ) ) ;
#4855=ORIENTED_EDGE ( 'NONE', *, *, #23082, .T. ) ;
#4863=EDGE_CURVE ( 'NONE', #19147, #11046, #21301, .T. ) ;
#4865=FACE_OUTER_BOUND ( 'NONE', #5562, .T. ) ;
#4869=EDGE_CURVE ( 'NONE', #2277, #824, #15934, .T. ) ;
#4873=CARTESIAN_POINT ( 'NONE',  ( -1.499999999960000219, 44.50000000000000000, -136.0552959530000123 ) ) ;
#4906=ORIENTED_EDGE ( 'NONE', *, *, #4304, .T. ) ;
#4912=DIRECTION ( 'NONE',  ( 0.000000000000000000, -1.000000000000000000, 0.000000000000000000 ) ) ;
#4931=VECTOR ( 'NONE', #23024, 1000.000000000000000 ) ;
#4938=CARTESIAN_POINT ( 'NONE',  ( -13.86630785130000021, 51.50000000000000000, -137.0552959530000123 ) ) ;
#4949=PRODUCT_DEFINITION_CONTEXT ( 'detailed design', #9462, 'design' ) ;
#4953=ORIENTED_EDGE ( 'NONE', *, *, #20582, .T. ) ;
#4956=EDGE_CURVE ( 'NONE', #4286, #21227, #10911, .T. ) ;
#4957=ORIENTED_EDGE ( 'NONE', *, *, #19000, .F. ) ;
#4968=CARTESIAN_POINT ( 'NONE',  ( 6.000000000010000001, -3.500000000000000000, -136.0552959530000123 ) ) ;
#4970=ORIENTED_EDGE ( 'NONE', *, *, #19000, .T. ) ;
#4991=LINE ( 'NONE', #8651, #13628 ) ;
#4998=EDGE_CURVE ( 'NONE', #10751, #18293, #18314, .T. ) ;
#5003=CARTESIAN_POINT ( 'NONE',  ( -15.19923223292398795, -41.50000000000003553, -136.0552959529657073 ) ) ;
#5011=ORIENTED_EDGE ( 'NONE', *, *, #2885, .T. ) ;
#5014=CARTESIAN_POINT ( 'NONE',  ( -4.499999999959999109, 40.00000000000000000, -136.0552959530000123 ) ) ;
#5025=AXIS2_PLACEMENT_3D ( 'NONE', #4590, #17084, #1161 ) ;
#5031=DIRECTION ( 'NONE',  ( 0.000000000000000000, -1.000000000000000000, 0.000000000000000000 ) ) ;
#5039=FACE_OUTER_BOUND ( 'NONE', #6999, .T. ) ;
#5040=CARTESIAN_POINT ( 'NONE',  ( 3.839256068031374536, -32.96302158184152375, -136.0552959530086525 ) ) ;
#5058=CARTESIAN_POINT ( 'NONE',  ( 4.750000000030000002, -44.75000000000000000, -136.0552959530000123 ) ) ;
#5059=CYLINDRICAL_SURFACE ( 'NONE', #23406, 2.000000000000001776 ) ;
#5091=ORIENTED_EDGE ( 'NONE', *, *, #19999, .T. ) ;
#5097=LINE ( 'NONE', #14614, #15947 ) ;
#5099=VERTEX_POINT ( 'NONE', #339 ) ;
#5101=CARTESIAN_POINT ( 'NONE',  ( -25.86630785129999666, -51.00000000000000000, -137.0552959530000123 ) ) ;
#5115=FACE_OUTER_BOUND ( 'NONE', #19090, .T. ) ;
#5119=VERTEX_POINT ( 'NONE', #22228 ) ;
#5124=CARTESIAN_POINT ( 'NONE',  ( -32.50000000000000000, -50.50000000000000000, -137.0552959530000123 ) ) ;
#5126=ORIENTED_EDGE ( 'NONE', *, *, #8066, .F. ) ;
#5131=ORIENTED_EDGE ( 'NONE', *, *, #17779, .F. ) ;
#5133=PLANE ( 'NONE',  #7444 ) ;
#5161=CARTESIAN_POINT ( 'NONE',  ( 8.750000000029995562, -45.01504245778616564, -136.0552959530197654 ) ) ;
#5167=VERTEX_POINT ( 'NONE', #3917 ) ;
#5185=CARTESIAN_POINT ( 'NONE',  ( -13.86630785130000021, -51.50000000000000000, -136.0552959530000123 ) ) ;
#5195=CARTESIAN_POINT ( 'NONE',  ( 3.000000000010000001, -3.500000000000000000, -136.5552959530000123 ) ) ;
#5202=VERTEX_POINT ( 'NONE', #17332 ) ;
#5205=DIRECTION ( 'NONE',  ( 2.255973186040000320E-12, 0.000000000000000000, 1.000000000000000000 ) ) ;
#5213=ORIENTED_EDGE ( 'NONE', *, *, #19694, .T. ) ;
#5217=ORIENTED_EDGE ( 'NONE', *, *, #1007, .F. ) ;
#5227=CARTESIAN_POINT ( 'NONE',  ( -0.9999999999639996862, 20.00701398444611101, -136.0552959529977954 ) ) ;
#5230=CARTESIAN_POINT ( 'NONE',  ( 3.611688725869999975E-11, 42.50000000000000000, -136.0552959530000123 ) ) ;
#5232=DIRECTION ( 'NONE',  ( 5.094701932209999624E-24, 1.000000000000000000, -1.149947916579999802E-35 ) ) ;
#5234=CARTESIAN_POINT ( 'NONE',  ( -7.499999999969999109, 42.50000000000000000, -137.0552959530000123 ) ) ;
#5236=DIRECTION ( 'NONE',  ( 2.257144641397284947E-12, 2.714724913984255017E-24, 1.000000000000000000 ) ) ;
#5242=EDGE_CURVE ( 'NONE', #19082, #14999, #16665, .T. ) ;
#5243=CYLINDRICAL_SURFACE ( 'NONE', #22405, 1.500000000000003331 ) ;
#5261=CARTESIAN_POINT ( 'NONE',  ( 8.701166446568034729, -31.45126136998390720, -136.0552959530196802 ) ) ;
#5265=ORIENTED_EDGE ( 'NONE', *, *, #3205, .T. ) ;
#5269=CARTESIAN_POINT ( 'NONE',  ( -5.098183173375419486, 20.66060904160994127, -136.0552959529885015 ) ) ;
#5285=SHAPE_DEFINITION_REPRESENTATION ( #15616, #6919 ) ;
#5288=VECTOR ( 'NONE', #15144, 1000.000000000000000 ) ;
#5290=CARTESIAN_POINT ( 'NONE',  ( 8.750000000030000891, -39.98606797749999942, -137.0552959530000123 ) ) ;
#5300=EDGE_CURVE ( 'NONE', #2454, #17032, #4610, .T. ) ;
#5307=EDGE_LOOP ( 'NONE', ( #8003, #11184, #15954, #13358 ) ) ;
#5308=CARTESIAN_POINT ( 'NONE',  ( 7.481747704286809686, 12.99999999999999645, -136.0552959530022008 ) ) ;
#5315=EDGE_CURVE ( 'NONE', #23517, #18273, #6623, .T. ) ;
#5317=CARTESIAN_POINT ( 'NONE',  ( 13.13369214870000157, 50.50000000000000000, -137.0552959530000123 ) ) ;
#5318=VECTOR ( 'NONE', #15565, 1000.000000000000000 ) ;
#5331=VERTEX_POINT ( 'NONE', #11727 ) ;
#5345=CARTESIAN_POINT ( 'NONE',  ( 13.13369214870000157, -2.273736754430000208E-12, -136.0552959530000123 ) ) ;
#5357=ORIENTED_EDGE ( 'NONE', *, *, #13877, .F. ) ;
#5366=LINE ( 'NONE', #1693, #17487 ) ;
#5373=FACE_OUTER_BOUND ( 'NONE', #1743, .T. ) ;
#5377=CARTESIAN_POINT ( 'NONE',  ( 4.500000000009999113, -2.000000000000000000, -136.0552959530000123 ) ) ;
#5393=B_SPLINE_CURVE_WITH_KNOTS ( 'NONE', 3,
 ( #9054, #8831, #20154, #10965, #16111, #5510, #7056, #14316, #3727, #21588, #16343, #21826, #5269, #1725, #18248, #12522, #8945, #19802 ),
 .UNSPECIFIED., .F., .F.,
 ( 4, 2, 2, 2, 2, 2, 2, 2, 4 ),
 ( 0.000000000000000000, 0.1250000000000000000, 0.2500000000000000000, 0.3750000000000000000, 0.5000000000000000000, 0.6250000000000000000, 0.7500000000000000000, 0.8750000000000000000, 1.000000000000000000 ),
 .UNSPECIFIED. ) ;
#5407=LINE ( 'NONE', #12405, #6797 ) ;
#5408=CARTESIAN_POINT ( 'NONE',  ( 20.50000000000000000, 19.50000000000000000, -136.5552959530000123 ) ) ;
#5409=B_SPLINE_CURVE_WITH_KNOTS ( 'NONE', 3,
 ( #7100, #8409, #15788, #19367, #17585, #14000, #1297, #21274, #23053, #4968 ),
 .UNSPECIFIED., .F., .F.,
 ( 4, 2, 2, 2, 4 ),
 ( 0.000000000000000000, 0.2500000000000000000, 0.5000000000000000000, 0.7500000000000000000, 1.000000000000000000 ),
 .UNSPECIFIED. ) ;
#5410=LINE ( 'NONE', #18136, #8363 ) ;
#5412=CYLINDRICAL_SURFACE ( 'NONE', #8201, 1.500000000000001998 ) ;
#5415=EDGE_CURVE ( 'NONE', #5167, #21713, #1495, .T. ) ;
#5421=VECTOR ( 'NONE', #14615, 1000.000000000000000 ) ;
#5423=EDGE_LOOP ( 'NONE', ( #22931, #14893, #717, #3015 ) ) ;
#5426=ORIENTED_EDGE ( 'NONE', *, *, #7638, .F. ) ;
#5427=CARTESIAN_POINT ( 'NONE',  ( 14.00000000000001421, 20.99298601554737331, -136.0552959530316173 ) ) ;
#5428=ORIENTED_EDGE ( 'NONE', *, *, #16317, .T. ) ;
#5447=ORIENTED_EDGE ( 'NONE', *, *, #2305, .F. ) ;
#5449=ORIENTED_EDGE ( 'NONE', *, *, #16484, .F. ) ;
#5461=EDGE_CURVE ( 'NONE', #8637, #12948, #5407, .T. ) ;
#5463=ORIENTED_EDGE ( 'NONE', *, *, #3986, .F. ) ;
#5486=CARTESIAN_POINT ( 'NONE',  ( -14.07817992003762697, -44.19950026359727957, -136.0552959530021155 ) ) ;
#5487=ORIENTED_EDGE ( 'NONE', *, *, #17383, .F. ) ;
#5508=CARTESIAN_POINT ( 'NONE',  ( 6.750000000030000002, -33.75000000000000000, -136.0552959530000123 ) ) ;
#5510=CARTESIAN_POINT ( 'NONE',  ( -5.098088255135088787, 24.33948587670753128, -136.0552959529885015 ) ) ;
#5518=CARTESIAN_POINT ( 'NONE',  ( -12.50000000000000000, 25.50000000000000000, -136.0552959530000123 ) ) ;
#5531=ORIENTED_EDGE ( 'NONE', *, *, #9466, .T. ) ;
#5537=CARTESIAN_POINT ( 'NONE',  ( 6.500000000040000003, 28.00000000000000000, -136.0552959530000123 ) ) ;
#5540=DIRECTION ( 'NONE',  ( 1.000000000000000000, -5.094701932209999624E-24, -2.257144641399999941E-12 ) ) ;
#5543=DIRECTION ( 'NONE',  ( -5.094701932209999624E-24, -1.000000000000000000, 1.149947916579999802E-35 ) ) ;
#5551=VECTOR ( 'NONE', #9515, 1000.000000000000000 ) ;
#5552=ORIENTED_EDGE ( 'NONE', *, *, #3201, .T. ) ;
#5553=DIRECTION ( 'NONE',  ( 0.000000000000000000, -1.000000000000000000, 0.000000000000000000 ) ) ;
#5562=EDGE_LOOP ( 'NONE', ( #12905, #7273, #4745, #14833 ) ) ;
#5565=DIRECTION ( 'NONE',  ( 1.000000000000000000, 0.000000000000000000, -2.257120985840000117E-12 ) ) ;
#5582=ORIENTED_EDGE ( 'NONE', *, *, #23057, .T. ) ;
#5616=DIRECTION ( 'NONE',  ( 2.257157423930000049E-12, 0.000000000000000000, 1.000000000000000000 ) ) ;
#5618=VECTOR ( 'NONE', #9868, 1000.000000000000000 ) ;
#5638=ORIENTED_EDGE ( 'NONE', *, *, #15794, .T. ) ;
#5643=CIRCLE ( 'NONE', #21997, 1.499999999999999556 ) ;
#5648=ORIENTED_EDGE ( 'NONE', *, *, #22317, .F. ) ;
#5652=DIRECTION ( 'NONE',  ( -1.000000000000000000, -7.105427357600000794E-15, 2.273736754430000208E-12 ) ) ;
#5654=FACE_BOUND ( 'NONE', #15792, .T. ) ;
#5657=CARTESIAN_POINT ( 'NONE',  ( 6.500000000030000002, 13.00000000000000000, -136.5552959530000123 ) ) ;
#5661=AXIS2_PLACEMENT_3D ( 'NONE', #2646, #9876, #8560 ) ;
#5698=EDGE_CURVE ( 'NONE', #6536, #20642, #7759, .T. ) ;
#5713=CARTESIAN_POINT ( 'NONE',  ( -3.499999999959999997, 42.50000000000000000, -136.0552959530000123 ) ) ;
#5717=ORIENTED_EDGE ( 'NONE', *, *, #8802, .F. ) ;
#5720=EDGE_CURVE ( 'NONE', #19082, #15679, #20738, .T. ) ;
#5721=ORIENTED_EDGE ( 'NONE', *, *, #11582, .F. ) ;
#5726=ORIENTED_EDGE ( 'NONE', *, *, #5300, .F. ) ;
#5747=VECTOR ( 'NONE', #22191, 1000.000000000000000 ) ;
#5753=CARTESIAN_POINT ( 'NONE',  ( -15.00000000000000000, -43.00000000000000000, -136.0552959530000123 ) ) ;
#5759=EDGE_LOOP ( 'NONE', ( #2474, #18937, #14357, #11505 ) ) ;
#5772=CARTESIAN_POINT ( 'NONE',  ( -15.00000000000000000, -43.00000000000000000, -136.0552959530000123 ) ) ;
#5776=ADVANCED_FACE ( 'NONE', ( #23344 ), #23229, .T. ) ;
#5777=DIRECTION ( 'NONE',  ( -1.000000000000000000, 0.000000000000000000, 2.257157423930000049E-12 ) ) ;
#5780=ORIENTED_EDGE ( 'NONE', *, *, #10942, .T. ) ;
#5796=DIRECTION ( 'NONE',  ( 2.257749542879999954E-12, 0.000000000000000000, 1.000000000000000000 ) ) ;
#5799=AXIS2_PLACEMENT_3D ( 'NONE', #631, #15019, #15263 ) ;
#5805=CARTESIAN_POINT ( 'NONE',  ( 19.13369214859999801, 50.50000000000000000, -136.0552959530000123 ) ) ;
#5817=CARTESIAN_POINT ( 'NONE',  ( 15.50000000000000000, 33.50000000000000000, -137.0552959530000123 ) ) ;
#5826=CARTESIAN_POINT ( 'NONE',  ( -4.726769794276915349, 42.89852487308498752, -136.0552959529893258 ) ) ;
#5830=CARTESIAN_POINT ( 'NONE',  ( -15.00000000000000000, -44.50000000000000000, -136.0552959530000123 ) ) ;
#5832=ORIENTED_EDGE ( 'NONE', *, *, #23057, .F. ) ;
#5834=APPLICATION_CONTEXT ( 'automotive_design' ) ;
#5852=B_SPLINE_CURVE_WITH_KNOTS ( 'NONE', 3,
 ( #21931, #16799, #22270, #7627, #14779, #16560, #268, #14900, #22158, #13215, #20490, #4191, #11425, #6203, #10346, #10105, #1094, #22733 ),
 .UNSPECIFIED., .F., .F.,
 ( 4, 2, 2, 2, 2, 2, 2, 2, 4 ),
 ( 0.000000000000000000, 0.1250000000000000000, 0.2500000000000000000, 0.3750000000000000000, 0.5000000000000000000, 0.6250000000000000000, 0.7500000000000000000, 0.8750000000000000000, 1.000000000000000000 ),
 .UNSPECIFIED. ) ;
#5873=ADVANCED_FACE ( 'NONE', ( #19782 ), #1346, .F. ) ;
#5874=EDGE_CURVE ( 'NONE', #16725, #4317, #8348, .T. ) ;
#5883=DIRECTION ( 'NONE',  ( -5.094701932209999624E-24, -1.000000000000000000, 1.149947916579999802E-35 ) ) ;
#5904=ORIENTED_EDGE ( 'NONE', *, *, #11945, .F. ) ;
#5927=CARTESIAN_POINT ( 'NONE',  ( -7.499999999959999997, 25.50000000000000000, -136.0552959530000123 ) ) ;
#5932=EDGE_CURVE ( 'NONE', #546, #8661, #20563, .T. ) ;
#5936=VECTOR ( 'NONE', #21126, 1000.000000000000000 ) ;
#5946=ORIENTED_EDGE ( 'NONE', *, *, #19571, .T. ) ;
#5948=CARTESIAN_POINT ( 'NONE',  ( -3.499999999959999997, 46.50000000000000000, -136.0552959530000123 ) ) ;
#5950=VERTEX_POINT ( 'NONE', #11496 ) ;
#5961=EDGE_CURVE ( 'NONE', #1387, #13267, #11295, .T. ) ;
#5993=DIRECTION ( 'NONE',  ( 0.000000000000000000, 1.000000000000000000, 0.000000000000000000 ) ) ;
#6000=DIRECTION ( 'NONE',  ( 5.094701932209999624E-24, 1.000000000000000000, -1.149947916579999802E-35 ) ) ;
#6007=FACE_OUTER_BOUND ( 'NONE', #1883, .T. ) ;
#6013=ORIENTED_EDGE ( 'NONE', *, *, #6506, .T. ) ;
#6015=ADVANCED_FACE ( 'NONE', ( #2377 ), #7153, .F. ) ;
#6043=ORIENTED_EDGE ( 'NONE', *, *, #7925, .F. ) ;
#6050=CARTESIAN_POINT ( 'NONE',  ( 4.500000000009999113, -3.500000000000000000, -137.0552959530000123 ) ) ;
#6058=VECTOR ( 'NONE', #12716, 1000.000000000000000 ) ;
#6065=ORIENTED_EDGE ( 'NONE', *, *, #13234, .T. ) ;
#6069=CARTESIAN_POINT ( 'NONE',  ( -4.020805332062283632, 42.55092418646380281, -136.0552959529909458 ) ) ;
#6074=ADVANCED_FACE ( 'NONE', ( #13780 ), #2598, .F. ) ;
#6084=VERTEX_POINT ( 'NONE', #21040 ) ;
#6093=LINE ( 'NONE', #4196, #12986 ) ;
#6101=EDGE_CURVE ( 'NONE', #15239, #14839, #15578, .T. ) ;
#6116=LINE ( 'NONE', #18846, #12202 ) ;
#6118=ORIENTED_EDGE ( 'NONE', *, *, #9151, .T. ) ;
#6129=FACE_BOUND ( 'NONE', #21175, .T. ) ;
#6139=EDGE_LOOP ( 'NONE', ( #18887, #8049, #21415, #14285 ) ) ;
#6141=EDGE_LOOP ( 'NONE', ( #19135, #12048, #21068, #2905 ) ) ;
#6142=LINE ( 'NONE', #6496, #8315 ) ;
#6144=CARTESIAN_POINT ( 'NONE',  ( 25.31684607429999900, -45.26810052439999765, -136.0552959530000123 ) ) ;
#6155=ORIENTED_EDGE ( 'NONE', *, *, #4400, .T. ) ;
#6160=CARTESIAN_POINT ( 'NONE',  ( 3.742473698254299652, -2.190250522973148595, -136.0552959530084536 ) ) ;
#6203=CARTESIAN_POINT ( 'NONE',  ( 13.66051412338692295, 38.90191174485966741, -136.0552959530308783 ) ) ;
#6236=LINE ( 'NONE', #18848, #11141 ) ;
#6238=CARTESIAN_POINT ( 'NONE',  ( -3.499999999969999998, 44.50000000000000000, -137.0552959530000123 ) ) ;
#6240=EDGE_LOOP ( 'NONE', ( #8866, #15575, #2931, #3867 ) ) ;
#6242=AXIS2_PLACEMENT_3D ( 'NONE', #23014, #22902, #6587 ) ;
#6245=DIRECTION ( 'NONE',  ( -1.000000000000000000, 5.094701932209999624E-24, 0.000000000000000000 ) ) ;
#6282=ORIENTED_EDGE ( 'NONE', *, *, #18279, .T. ) ;
#6307=VECTOR ( 'NONE', #15092, 1000.000000000000000 ) ;
#6320=ORIENTED_EDGE ( 'NONE', *, *, #8719, .T. ) ;
#6322=DIRECTION ( 'NONE',  ( 2.255973186040000320E-12, 0.000000000000000000, 1.000000000000000000 ) ) ;
#6323=EDGE_CURVE ( 'NONE', #16131, #13781, #8752, .T. ) ;
#6330=CARTESIAN_POINT ( 'NONE',  ( -15.00000000000000000, -44.50000000000000000, -136.5552959530000123 ) ) ;
#6333=ADVANCED_FACE ( 'NONE', ( #8872 ), #18633, .T. ) ;
#6335=ADVANCED_FACE ( 'NONE', ( #15055 ), #20069, .T. ) ;
#6344=EDGE_LOOP ( 'NONE', ( #11566, #9276, #12901, #20824 ) ) ;
#6351=ORIENTED_EDGE ( 'NONE', *, *, #19721, .F. ) ;
#6363=DIRECTION ( 'NONE',  ( 5.094701932209999624E-24, 1.000000000000000000, 0.000000000000000000 ) ) ;
#6364=ORIENTED_EDGE ( 'NONE', *, *, #18526, .F. ) ;
#6373=LINE ( 'NONE', #15311, #19781 ) ;
#6383=DIRECTION ( 'NONE',  ( -1.000000000000000000, 0.000000000000000000, 2.257120985840000117E-12 ) ) ;
#6387=VECTOR ( 'NONE', #21637, 1000.000000000000000 ) ;
#6402=AXIS2_PLACEMENT_3D ( 'NONE', #21156, #17216, #931 ) ;
#6436=FACE_OUTER_BOUND ( 'NONE', #14109, .T. ) ;
#6438=CARTESIAN_POINT ( 'NONE',  ( -32.50000000000000000, 47.50000000000000000, -136.5552959530000123 ) ) ;
#6445=FACE_OUTER_BOUND ( 'NONE', #939, .T. ) ;
#6473=LINE ( 'NONE', #12398, #9638 ) ;
#6482=EDGE_CURVE ( 'NONE', #11395, #11936, #8496, .T. ) ;
#6485=VECTOR ( 'NONE', #18096, 1000.000000000000000 ) ;
#6496=CARTESIAN_POINT ( 'NONE',  ( 31.50000000010000178, -40.03620104880000241, -136.5552959530000123 ) ) ;
#6497=ORIENTED_EDGE ( 'NONE', *, *, #17383, .T. ) ;
#6499=VECTOR ( 'NONE', #6855, 1000.000000000000000 ) ;
#6506=EDGE_CURVE ( 'NONE', #22598, #12804, #10743, .T. ) ;
#6518=ORIENTED_EDGE ( 'NONE', *, *, #11582, .T. ) ;
#6534=VECTOR ( 'NONE', #16564, 1000.000000000000000 ) ;
#6536=VERTEX_POINT ( 'NONE', #17668 ) ;
#6552=DIRECTION ( 'NONE',  ( 2.257144641399999941E-12, -8.049635416090000264E-35, 1.000000000000000000 ) ) ;
#6574=CARTESIAN_POINT ( 'NONE',  ( 20.50000000000000000, 25.50000000000000000, -137.0552959530000123 ) ) ;
#6587=DIRECTION ( 'NONE',  ( 0.7071067811865473507, 0.7071067811865476838, -1.591319668629389897E-12 ) ) ;
#6607=ORIENTED_EDGE ( 'NONE', *, *, #1995, .T. ) ;
#6623=LINE ( 'NONE', #3072, #18206 ) ;
#6625=CARTESIAN_POINT ( 'NONE',  ( -13.50000000000000000, -43.00000000000000000, -137.0552959530000123 ) ) ;
#6635=VERTEX_POINT ( 'NONE', #14922 ) ;
#6649=CARTESIAN_POINT ( 'NONE',  ( -25.86630785129999666, -50.50000000000000000, -136.5552959530000123 ) ) ;
#6652=FACE_OUTER_BOUND ( 'NONE', #8019, .T. ) ;
#6664=CARTESIAN_POINT ( 'NONE',  ( -12.50000000000000000, 48.50000000000000000, -136.5552959530000123 ) ) ;
#6668=FACE_OUTER_BOUND ( 'NONE', #19252, .T. ) ;
#6683=EDGE_CURVE ( 'NONE', #20086, #17769, #532, .T. ) ;
#6686=CARTESIAN_POINT ( 'NONE',  ( 32.00000000000000000, 32.96379895120000469, -137.0552959530000123 ) ) ;
#6716=EDGE_CURVE ( 'NONE', #5950, #4170, #20171, .T. ) ;
#6724=ORIENTED_EDGE ( 'NONE', *, *, #15661, .T. ) ;
#6725=CARTESIAN_POINT ( 'NONE',  ( 3.611688725869999975E-11, 21.50000000000000000, -136.0552959530000123 ) ) ;
#6729=VERTEX_POINT ( 'NONE', #4679 ) ;
#6730=LINE ( 'NONE', #10409, #1139 ) ;
#6736=ORIENTED_EDGE ( 'NONE', *, *, #11945, .T. ) ;
#6739=CARTESIAN_POINT ( 'NONE',  ( 31.50000000000000000, 40.03620104880000241, -136.0552959530000123 ) ) ;
#6748=VERTEX_POINT ( 'NONE', #6574 ) ;
#6749=DIRECTION ( 'NONE',  ( 0.000000000000000000, -1.000000000000000000, 0.000000000000000000 ) ) ;
#6751=ORIENTED_EDGE ( 'NONE', *, *, #18061, .F. ) ;
#6778=VECTOR ( 'NONE', #2655, 1000.000000000000000 ) ;
#6797=VECTOR ( 'NONE', #14450, 1000.000000000000000 ) ;
#6798=VECTOR ( 'NONE', #8112, 1000.000000000000000 ) ;
#6838=AXIS2_PLACEMENT_3D ( 'NONE', #20762, #13735, #1016 ) ;
#6841=EDGE_LOOP ( 'NONE', ( #15409, #2575, #247, #10506 ) ) ;
#6855=DIRECTION ( 'NONE',  ( 2.256861364460000137E-12, 0.000000000000000000, 1.000000000000000000 ) ) ;
#6856=CIRCLE ( 'NONE', #1942, 1.500000000000001332 ) ;
#6879=DIRECTION ( 'NONE',  ( 1.000000000000000000, 0.000000000000000000, -2.257453483404485639E-12 ) ) ;
#6885=DIRECTION ( 'NONE',  ( 2.255973186040000320E-12, 0.000000000000000000, 1.000000000000000000 ) ) ;
#6903=EDGE_CURVE ( 'NONE', #7002, #17964, #1246, .T. ) ;
#6905=ORIENTED_EDGE ( 'NONE', *, *, #1982, .F. ) ;
#6916=CYLINDRICAL_SURFACE ( 'NONE', #9204, 1.500000000000001332 ) ;
#6917=DIRECTION ( 'NONE',  ( -1.000000000000000000, 0.000000000000000000, 2.257495777610000006E-12 ) ) ;
#6919=SHAPE_REPRESENTATION ( 'Cover Plate', ( #5025 ), #1616 ) ;
#6927=CARTESIAN_POINT ( 'NONE',  ( -6.366307851350000213, 50.50000000000000000, -137.0552959530000123 ) ) ;
#6930=ORIENTED_EDGE ( 'NONE', *, *, #3076, .F. ) ;
#6934=CARTESIAN_POINT ( 'NONE',  ( 22.50000000000000000, 33.50000000000000000, -136.0552959530000123 ) ) ;
#6935=CARTESIAN_POINT ( 'NONE',  ( 8.976561295290075293, -35.78342539458139271, -136.0552959530202770 ) ) ;
#6939=ORIENTED_EDGE ( 'NONE', *, *, #9178, .F. ) ;
#6946=CARTESIAN_POINT ( 'NONE',  ( -3.499999999959999997, 40.00000000000000000, -136.0552959530000123 ) ) ;
#6947=ORIENTED_EDGE ( 'NONE', *, *, #18138, .F. ) ;
#6956=CARTESIAN_POINT ( 'NONE',  ( -1.900666315163639597, 43.27090656005016456, -136.0552959530036219 ) ) ;
#6958=CARTESIAN_POINT ( 'NONE',  ( -13.50000000000000000, -43.00000000000000000, -136.0552959530000123 ) ) ;
#6963=( NAMED_UNIT ( * ) SI_UNIT ( $, .STERADIAN. ) SOLID_ANGLE_UNIT ( ) );
#6964=VERTEX_POINT ( 'NONE', #3355 ) ;
#6967=ORIENTED_EDGE ( 'NONE', *, *, #13158, .F. ) ;
#6970=CARTESIAN_POINT ( 'NONE',  ( 22.89765167460447870, 39.50000000000002842, -136.0552959530517398 ) ) ;
#6999=EDGE_LOOP ( 'NONE', ( #16415, #2791, #10914, #4335 ) ) ;
#7001=LINE ( 'NONE', #12585, #23271 ) ;
#7002=VERTEX_POINT ( 'NONE', #19548 ) ;
#7008=ORIENTED_EDGE ( 'NONE', *, *, #2068, .T. ) ;
#7009=LINE ( 'NONE', #3324, #4445 ) ;
#7010=CARTESIAN_POINT ( 'NONE',  ( 31.50000000000000000, -21.03620104879999886, -137.0552959530000123 ) ) ;
#7014=CARTESIAN_POINT ( 'NONE',  ( 1.544882029700253234, 14.84887268567989338, -136.0552959530035082 ) ) ;
#7031=CARTESIAN_POINT ( 'NONE',  ( 32.00000000000000000, 20.96379895120000114, -136.0552959530000123 ) ) ;
#7043=DIRECTION ( 'NONE',  ( 0.000000000000000000, 1.000000000000000000, 0.000000000000000000 ) ) ;
#7046=DIRECTION ( 'NONE',  ( -1.000000000000000000, 1.156482317317871331E-15, 2.257453483404484831E-12 ) ) ;
#7049=CARTESIAN_POINT ( 'NONE',  ( 17.57628698946902901, 21.71923945895291652, -136.0552959530396890 ) ) ;
#7056=CARTESIAN_POINT ( 'NONE',  ( -4.881030538545268804, 24.01480899505181554, -136.0552959529889847 ) ) ;
#7058=EDGE_LOOP ( 'NONE', ( #10727, #12467, #2139, #13469 ) ) ;
#7062=VECTOR ( 'NONE', #21723, 1000.000000000000000 ) ;
#7064=FACE_OUTER_BOUND ( 'NONE', #6139, .T. ) ;
#7072=EDGE_CURVE ( 'NONE', #18341, #4286, #16790, .T. ) ;
#7076=CARTESIAN_POINT ( 'NONE',  ( -1.499999999959999331, 44.23820061220084199, -136.0552959530045314 ) ) ;
#7087=ORIENTED_EDGE ( 'NONE', *, *, #6903, .T. ) ;
#7100=CARTESIAN_POINT ( 'NONE',  ( 4.500000000009999113, -5.000000000000000000, -136.0552959530000123 ) ) ;
#7116=CARTESIAN_POINT ( 'NONE',  ( 19.13369214859999801, -50.50000000000000000, -136.0552959530000123 ) ) ;
#7120=DIRECTION ( 'NONE',  ( 1.000000000000000000, 0.000000000000000000, -2.257453483404482811E-12 ) ) ;
#7121=LINE ( 'NONE', #5345, #19386 ) ;
#7124=VERTEX_POINT ( 'NONE', #12744 ) ;
#7133=VERTEX_POINT ( 'NONE', #20017 ) ;
#7146=CARTESIAN_POINT ( 'NONE',  ( -14.60737817346108258, -44.46095901500248004, -136.0552959530008934 ) ) ;
#7147=ORIENTED_EDGE ( 'NONE', *, *, #1878, .F. ) ;
#7153=PLANE ( 'NONE',  #750 ) ;
#7155=DIRECTION ( 'NONE',  ( -1.000000000000000000, 5.094701932209999624E-24, 2.257144641399999941E-12 ) ) ;
#7158=CIRCLE ( 'NONE', #20096, 2.000000000000000000 ) ;
#7166=ORIENTED_EDGE ( 'NONE', *, *, #5932, .F. ) ;
#7167=CARTESIAN_POINT ( 'NONE',  ( 18.98502865247582960, 25.11890206003844384, -136.0552959530428723 ) ) ;
#7170=DIRECTION ( 'NONE',  ( -2.891205793294675861E-15, -1.000000000000000000, 0.000000000000000000 ) ) ;
#7185=CARTESIAN_POINT ( 'NONE',  ( 8.496192186321144035, -45.75965300677037106, -136.0552959530191970 ) ) ;
#7191=DIRECTION ( 'NONE',  ( -5.094701932209999624E-24, -1.000000000000000000, 1.149947916579999802E-35 ) ) ;
#7221=CARTESIAN_POINT ( 'NONE',  ( -15.50000000000000000, 47.50000000000000000, -136.5552959530000123 ) ) ;
#7239=AXIS2_PLACEMENT_3D ( 'NONE', #21080, #17376, #3220 ) ;
#7244=CARTESIAN_POINT ( 'NONE',  ( 25.50000000000000000, 19.50000000000000000, -136.0552959530000123 ) ) ;
#7251=AXIS2_PLACEMENT_3D ( 'NONE', #8222, #1111, #10121 ) ;
#7259=CARTESIAN_POINT ( 'NONE',  ( 6.000000000010000001, -3.500000000000000000, -136.5552959530000123 ) ) ;
#7266=DIRECTION ( 'NONE',  ( -1.000000000000000000, 5.094701932209999624E-24, 2.257144641399999941E-12 ) ) ;
#7273=ORIENTED_EDGE ( 'NONE', *, *, #22784, .F. ) ;
#7290=CARTESIAN_POINT ( 'NONE',  ( 3.775218130429260022, -33.25714246578316136, -136.0552959530085673 ) ) ;
#7326=CARTESIAN_POINT ( 'NONE',  ( -3.499999999969999998, 44.50000000000000000, -137.0552959530000123 ) ) ;
#7342=ORIENTED_EDGE ( 'NONE', *, *, #21957, .F. ) ;
#7363=ADVANCED_FACE ( 'NONE', ( #9481 ), #20569, .F. ) ;
#7369=DIRECTION ( 'NONE',  ( 1.000000000000000000, 0.000000000000000000, -2.257018101830000309E-12 ) ) ;
#7378=CARTESIAN_POINT ( 'NONE',  ( -15.50000000000000000, 21.50000000000000000, -137.0552959530000123 ) ) ;
#7384=CARTESIAN_POINT ( 'NONE',  ( -13.49999999999999645, -43.19634954084936140, -136.0552959530033945 ) ) ;
#7392=ORIENTED_EDGE ( 'NONE', *, *, #18810, .F. ) ;
#7415=VECTOR ( 'NONE', #4647, 1000.000000000000000 ) ;
#7424=CARTESIAN_POINT ( 'NONE',  ( -32.50000000000000000, -50.50000000000000000, -136.5552959530000123 ) ) ;
#7427=ORIENTED_EDGE ( 'NONE', *, *, #2686, .F. ) ;
#7431=CARTESIAN_POINT ( 'NONE',  ( 25.00000000000000000, -20.50000000000000000, -137.0552959530000123 ) ) ;
#7435=LINE ( 'NONE', #14698, #20093 ) ;
#7436=VERTEX_POINT ( 'NONE', #16363 ) ;
#7437=FACE_BOUND ( 'NONE', #13944, .T. ) ;
#7442=CIRCLE ( 'NONE', #21134, 7.499999999999999112 ) ;
#7444=AXIS2_PLACEMENT_3D ( 'NONE', #12384, #1245, #15736 ) ;
#7447=ORIENTED_EDGE ( 'NONE', *, *, #21957, .T. ) ;
#7448=CARTESIAN_POINT ( 'NONE',  ( -12.50000000000000000, 19.50000000000000000, -136.5552959530000123 ) ) ;
#7449=VERTEX_POINT ( 'NONE', #5290 ) ;
#7455=EDGE_LOOP ( 'NONE', ( #11520, #20571, #15880, #22113 ) ) ;
#7458=ORIENTED_EDGE ( 'NONE', *, *, #8925, .F. ) ;
#7477=VERTEX_POINT ( 'NONE', #1857 ) ;
#7487=ADVANCED_FACE ( 'NONE', ( #21728 ), #18028, .T. ) ;
#7488=DIRECTION ( 'NONE',  ( 1.000000000000000000, 0.000000000000000000, -2.257453483404482811E-12 ) ) ;
#7494=AXIS2_PLACEMENT_3D ( 'NONE', #8963, #1184, #1740 ) ;
#7495=VERTEX_POINT ( 'NONE', #6958 ) ;
#7509=VECTOR ( 'NONE', #22388, 1000.000000000000000 ) ;
#7513=CARTESIAN_POINT ( 'NONE',  ( 8.250000000030000891, -37.98606797749999942, -137.0552959530000123 ) ) ;
#7514=EDGE_CURVE ( 'NONE', #4286, #1507, #21044, .T. ) ;
#7521=CARTESIAN_POINT ( 'NONE',  ( -2.499999999959999997, 34.00000000000000000, -136.0552959530000123 ) ) ;
#7528=DIRECTION ( 'NONE',  ( 5.094701932209999624E-24, 1.000000000000000000, -1.149947916579999802E-35 ) ) ;
#7543=DIRECTION ( 'NONE',  ( -0.6459422414661292189, -0.7633862853691524286, 1.457985068980290749E-12 ) ) ;
#7556=DIRECTION ( 'NONE',  ( -2.257144641399999941E-12, 0.000000000000000000, -1.000000000000000000 ) ) ;
#7572=VECTOR ( 'NONE', #15024, 1000.000000000000000 ) ;
#7595=VECTOR ( 'NONE', #2561, 1000.000000000000000 ) ;
#7618=EDGE_CURVE ( 'NONE', #11046, #13504, #16934, .T. ) ;
#7623=VERTEX_POINT ( 'NONE', #293 ) ;
#7627=CARTESIAN_POINT ( 'NONE',  ( 13.98537695664809277, 33.88080765318336063, -136.0552959530315320 ) ) ;
#7628=EDGE_CURVE ( 'NONE', #824, #12377, #3865, .T. ) ;
#7638=EDGE_CURVE ( 'NONE', #11916, #1387, #10142, .T. ) ;
#7646=VECTOR ( 'NONE', #14173, 1000.000000000000000 ) ;
#7666=CARTESIAN_POINT ( 'NONE',  ( 22.50000000000000000, 33.50000000000000000, -136.0552959530000123 ) ) ;
#7668=FACE_OUTER_BOUND ( 'NONE', #14207, .T. ) ;
#7683=EDGE_LOOP ( 'NONE', ( #19102, #9478, #6967, #16496 ) ) ;
#7694=AXIS2_PLACEMENT_3D ( 'NONE', #4319, #20850, #19062 ) ;
#7707=DIRECTION ( 'NONE',  ( 5.094701932209999624E-24, 1.000000000000000000, 0.000000000000000000 ) ) ;
#7709=ORIENTED_EDGE ( 'NONE', *, *, #16087, .T. ) ;
#7714=CARTESIAN_POINT ( 'NONE',  ( -15.50000000000000000, 21.50000000000000000, -136.5552959530000123 ) ) ;
#7723=VERTEX_POINT ( 'NONE', #14078 ) ;
#7726=ADVANCED_FACE ( 'NONE', ( #5039 ), #12279, .F. ) ;
#7727=CARTESIAN_POINT ( 'NONE',  ( -5.499999999959999997, 44.50000000000000000, -136.0552959530000123 ) ) ;
#7733=VERTEX_POINT ( 'NONE', #6934 ) ;
#7744=ADVANCED_FACE ( 'NONE', ( #12389 ), #14195, .F. ) ;
#7752=ORIENTED_EDGE ( 'NONE', *, *, #13707, .T. ) ;
#7759=LINE ( 'NONE', #13231, #5288 ) ;
#7762=CARTESIAN_POINT ( 'NONE',  ( 32.50000000000000000, 32.96379895120000469, -136.5552959530000123 ) ) ;
#7779=CARTESIAN_POINT ( 'NONE',  ( -16.50000000000000000, -43.00000000000000000, -136.5552959530000123 ) ) ;
#7788=EDGE_LOOP ( 'NONE', ( #21147, #8365, #2815, #9970 ) ) ;
#7814=VECTOR ( 'NONE', #886, 1000.000000000000000 ) ;
#7825=DIRECTION ( 'NONE',  ( -2.257144641399999941E-12, 8.049635416090000264E-35, -1.000000000000000000 ) ) ;
#7834=VERTEX_POINT ( 'NONE', #9523 ) ;
#7840=CARTESIAN_POINT ( 'NONE',  ( -2.273230205652897240, 46.10147512692442717, -136.0552959529948680 ) ) ;
#7850=CARTESIAN_POINT ( 'NONE',  ( -32.50000000000000000, -2.273736754430000208E-12, -136.0552959530000123 ) ) ;
#7886=VECTOR ( 'NONE', #14168, 1000.000000000000000 ) ;
#7887=ORIENTED_EDGE ( 'NONE', *, *, #21481, .F. ) ;
#7888=LINE ( 'NONE', #15167, #15201 ) ;
#7913=DIRECTION ( 'NONE',  ( 2.257144641401724984E-12, 0.000000000000000000, 1.000000000000000000 ) ) ;
#7921=VECTOR ( 'NONE', #18019, 1000.000000000000000 ) ;
#7925=EDGE_CURVE ( 'NONE', #1756, #7449, #15363, .T. ) ;
#7929=ORIENTED_EDGE ( 'NONE', *, *, #9151, .F. ) ;
#7939=ORIENTED_EDGE ( 'NONE', *, *, #905, .T. ) ;
#7951=EDGE_LOOP ( 'NONE', ( #21585, #1442, #6118, #21195 ) ) ;
#7962=CIRCLE ( 'NONE', #15967, 2.000000000000000000 ) ;
#7980=CARTESIAN_POINT ( 'NONE',  ( -32.50000000000000000, -2.273736754430000208E-12, -136.0552959530000123 ) ) ;
#8003=ORIENTED_EDGE ( 'NONE', *, *, #16525, .T. ) ;
#8015=FACE_OUTER_BOUND ( 'NONE', #12087, .T. ) ;
#8019=EDGE_LOOP ( 'NONE', ( #1592, #13787, #8529, #21823 ) ) ;
#8030=CARTESIAN_POINT ( 'NONE',  ( 19.13369214859999801, -50.50000000000000000, -137.0552959530000123 ) ) ;
#8037=FACE_OUTER_BOUND ( 'NONE', #14841, .T. ) ;
#8038=CARTESIAN_POINT ( 'NONE',  ( -12.50000000000000000, -2.273736754430000208E-12, -136.0552959530000123 ) ) ;
#8047=FACE_OUTER_BOUND ( 'NONE', #4723, .T. ) ;
#8049=ORIENTED_EDGE ( 'NONE', *, *, #8382, .T. ) ;
#8066=EDGE_CURVE ( 'NONE', #6964, #7124, #14046, .T. ) ;
#8074=ORIENTED_EDGE ( 'NONE', *, *, #10170, .T. ) ;
#8078=CARTESIAN_POINT ( 'NONE',  ( -15.75743038489378200, -44.30994315220375057, -136.0552959529644568 ) ) ;
#8089=VERTEX_POINT ( 'NONE', #12480 ) ;
#8105=ORIENTED_EDGE ( 'NONE', *, *, #417, .T. ) ;
#8112=DIRECTION ( 'NONE',  ( 0.000000000000000000, 1.000000000000000000, 0.000000000000000000 ) ) ;
#8129=VERTEX_POINT ( 'NONE', #21198 ) ;
#8134=DIRECTION ( 'NONE',  ( -5.094701932209999624E-24, -1.000000000000000000, 1.149947916579999802E-35 ) ) ;
#8136=FACE_OUTER_BOUND ( 'NONE', #7683, .T. ) ;
#8139=DIRECTION ( 'NONE',  ( 1.000000000000000000, -5.094701932209999624E-24, 0.000000000000000000 ) ) ;
#8143=ORIENTED_EDGE ( 'NONE', *, *, #16811, .T. ) ;
#8145=CARTESIAN_POINT ( 'NONE',  ( 3.611688725869999975E-11, 50.50000000000000000, -136.0552959530000123 ) ) ;
#8171=FACE_OUTER_BOUND ( 'NONE', #14295, .T. ) ;
#8173=DIRECTION ( 'NONE',  ( -1.000000000000000000, 5.094701932209999624E-24, 2.257144641399999941E-12 ) ) ;
#8175=ORIENTED_EDGE ( 'NONE', *, *, #15661, .F. ) ;
#8178=EDGE_LOOP ( 'NONE', ( #3944, #18391, #23174, #3408 ) ) ;
#8186=VERTEX_POINT ( 'NONE', #5817 ) ;
#8201=AXIS2_PLACEMENT_3D ( 'NONE', #5753, #21599, #21948 ) ;
#8208=ORIENTED_EDGE ( 'NONE', *, *, #3416, .T. ) ;
#8215=DIRECTION ( 'NONE',  ( 1.000000000000000000, 0.000000000000000000, -2.273736754430000208E-12 ) ) ;
#8222=CARTESIAN_POINT ( 'NONE',  ( -7.499999999969999109, 22.50000000000000000, -137.0552959530000123 ) ) ;
#8235=EDGE_CURVE ( 'NONE', #17964, #7834, #2265, .T. ) ;
#8236=VECTOR ( 'NONE', #12188, 1000.000000000000000 ) ;
#8242=CARTESIAN_POINT ( 'NONE',  ( 6.750000000030000002, -44.75000000000000000, -137.0552959530000123 ) ) ;
#8250=FACE_BOUND ( 'NONE', #22444, .T. ) ;
#8260=EDGE_LOOP ( 'NONE', ( #18872, #4361, #9756, #17486 ) ) ;
#8262=EDGE_LOOP ( 'NONE', ( #22481, #5426, #9842, #20423 ) ) ;
#8266=CARTESIAN_POINT ( 'NONE',  ( 5.519240656430695502, 27.95201674008767156, -136.0552959530124895 ) ) ;
#8278=VECTOR ( 'NONE', #6885, 1000.000000000000000 ) ;
#8282=ORIENTED_EDGE ( 'NONE', *, *, #13526, .F. ) ;
#8289=DIRECTION ( 'NONE',  ( 1.000000000000000000, 0.000000000000000000, -2.257453483404485235E-12 ) ) ;
#8291=DIRECTION ( 'NONE',  ( -2.257144641399999941E-12, 8.049635416090000264E-35, -1.000000000000000000 ) ) ;
#8294=DIRECTION ( 'NONE',  ( 5.094701932209999624E-24, 1.000000000000000000, 0.000000000000000000 ) ) ;
#8296=ORIENTED_EDGE ( 'NONE', *, *, #907, .T. ) ;
#8301=AXIS2_PLACEMENT_3D ( 'NONE', #7378, #5232, #23444 ) ;
#8315=VECTOR ( 'NONE', #20779, 1000.000000000000000 ) ;
#8319=CARTESIAN_POINT ( 'NONE',  ( -16.20103055061850839, -42.07987191916137704, -136.0552959529634620 ) ) ;
#8340=ORIENTED_EDGE ( 'NONE', *, *, #15670, .F. ) ;
#8348=LINE ( 'NONE', #17517, #12122 ) ;
#8356=DIRECTION ( 'NONE',  ( 2.257157423930000049E-12, 0.000000000000000000, 1.000000000000000000 ) ) ;
#8361=CIRCLE ( 'NONE', #20156, 2.000000000000000888 ) ;
#8362=DIRECTION ( 'NONE',  ( 1.000000000000000000, 0.000000000000000000, -2.257453483404482811E-12 ) ) ;
#8363=VECTOR ( 'NONE', #407, 1000.000000000000000 ) ;
#8365=ORIENTED_EDGE ( 'NONE', *, *, #4998, .T. ) ;
#8368=CYLINDRICAL_SURFACE ( 'NONE', #6242, 1.500000000000001110 ) ;
#8377=EDGE_CURVE ( 'NONE', #21090, #17829, #15951, .T. ) ;
#8382=EDGE_CURVE ( 'NONE', #21201, #2271, #22703, .T. ) ;
#8391=VERTEX_POINT ( 'NONE', #17228 ) ;
#8409=CARTESIAN_POINT ( 'NONE',  ( 4.696349540859360516, -5.000000000000000000, -136.0552959530004387 ) ) ;
#8414=CARTESIAN_POINT ( 'NONE',  ( 13.13369214870000157, -50.50000000000000000, -136.5552959530000123 ) ) ;
#8420=CARTESIAN_POINT ( 'NONE',  ( 32.50000000000000000, 20.96379895120000114, -136.5552959530000123 ) ) ;
#8434=EDGE_CURVE ( 'NONE', #8186, #16725, #4552, .T. ) ;
#8444=( GEOMETRIC_REPRESENTATION_CONTEXT ( 3 ) GLOBAL_UNCERTAINTY_ASSIGNED_CONTEXT ( ( #19693 ) ) GLOBAL_UNIT_ASSIGNED_CONTEXT ( ( #14228, #19474, #6963 ) ) REPRESENTATION_CONTEXT ( 'NONE', 'WORKASPACE' ) );
#8447=DIRECTION ( 'NONE',  ( 2.259525899719999991E-12, 0.000000000000000000, 1.000000000000000000 ) ) ;
#8459=DIRECTION ( 'NONE',  ( 1.000000000000000000, 0.000000000000000000, -2.257120985840000117E-12 ) ) ;
#8488=EDGE_CURVE ( 'NONE', #7449, #4637, #4498, .T. ) ;
#8493=CARTESIAN_POINT ( 'NONE',  ( 6.485119744368450512, -46.75006725843203981, -136.0552959530146211 ) ) ;
#8496=LINE ( 'NONE', #18142, #15085 ) ;
#8516=DIRECTION ( 'NONE',  ( 0.000000000000000000, 1.000000000000000000, 0.000000000000000000 ) ) ;
#8526=ORIENTED_EDGE ( 'NONE', *, *, #608, .T. ) ;
#8529=ORIENTED_EDGE ( 'NONE', *, *, #16678, .T. ) ;
#8537=LINE ( 'NONE', #13545, #13778 ) ;
#8543=ORIENTED_EDGE ( 'NONE', *, *, #4400, .F. ) ;
#8548=ORIENTED_EDGE ( 'NONE', *, *, #4869, .F. ) ;
#8554=EDGE_CURVE ( 'NONE', #16332, #10697, #15801, .T. ) ;
#8555=CARTESIAN_POINT ( 'NONE',  ( -3.499999999969999998, 44.50000000000000000, -137.0552959530000123 ) ) ;
#8557=VECTOR ( 'NONE', #16385, 1000.000000000000000 ) ;
#8560=DIRECTION ( 'NONE',  ( -1.000000000000000000, 5.094701932209999624E-24, 0.000000000000000000 ) ) ;
#8564=ORIENTED_EDGE ( 'NONE', *, *, #13707, .F. ) ;
#8599=ADVANCED_FACE ( 'NONE', ( #13859, #8250, #6129, #19208, #4234, #11469, #18748, #2802, #13615, #662, #15173, #8015 ), #15523, .T. ) ;
#8616=DIRECTION ( 'NONE',  ( 0.000000000000000000, 1.603797727360000188E-26, -1.000000000000000000 ) ) ;
#8617=EDGE_CURVE ( 'NONE', #14599, #7436, #17068, .T. ) ;
#8621=PLANE ( 'NONE',  #12737 ) ;
#8628=CARTESIAN_POINT ( 'NONE',  ( 3.611688725869999975E-11, 51.50000000000000000, -136.0552959530000123 ) ) ;
#8634=VERTEX_POINT ( 'NONE', #4938 ) ;
#8636=CARTESIAN_POINT ( 'NONE',  ( -15.50000000000000000, 21.50000000000000000, -137.0552959530000123 ) ) ;
#8637=VERTEX_POINT ( 'NONE', #10497 ) ;
#8643=ORIENTED_EDGE ( 'NONE', *, *, #9226, .F. ) ;
#8646=CARTESIAN_POINT ( 'NONE',  ( 15.50000000000000000, 36.50000000000000000, -136.0552959530000123 ) ) ;
#8650=VECTOR ( 'NONE', #644, 1000.000000000000000 ) ;
#8651=CARTESIAN_POINT ( 'NONE',  ( 3.611688725869999975E-11, 40.00000000000000000, -136.0552959530000123 ) ) ;
#8660=DIRECTION ( 'NONE',  ( 0.000000000000000000, -1.000000000000000000, 0.000000000000000000 ) ) ;
#8661=VERTEX_POINT ( 'NONE', #19811 ) ;
#8664=VECTOR ( 'NONE', #12790, 1000.000000000000000 ) ;
#8671=DIRECTION ( 'NONE',  ( -1.000000000000000000, 5.094701932209999624E-24, 2.257144641399999941E-12 ) ) ;
#8672=CARTESIAN_POINT ( 'NONE',  ( -13.50000000000000711, -42.80076776703756281, -136.0552959529695158 ) ) ;
#8679=CARTESIAN_POINT ( 'NONE',  ( 6.500000000040000003, 20.50000000000000000, -136.0552959530000123 ) ) ;
#8684=AXIS2_PLACEMENT_3D ( 'NONE', #4626, #8173, #8294 ) ;
#8710=VECTOR ( 'NONE', #6749, 1000.000000000000000 ) ;
#8719=EDGE_CURVE ( 'NONE', #17721, #20642, #4755, .T. ) ;
#8728=VECTOR ( 'NONE', #19349, 1000.000000000000000 ) ;
#8734=SURFACE_SIDE_STYLE ('',( #1511 ) ) ;
#8740=VERTEX_POINT ( 'NONE', #12300 ) ;
#8746=EDGE_LOOP ( 'NONE', ( #6065, #19604, #5217, #839 ) ) ;
#8752=LINE ( 'NONE', #8628, #22309 ) ;
#8757=ORIENTED_EDGE ( 'NONE', *, *, #5315, .F. ) ;
#8761=ORIENTED_EDGE ( 'NONE', *, *, #16598, .F. ) ;
#8772=ORIENTED_EDGE ( 'NONE', *, *, #2859, .F. ) ;
#8787=CARTESIAN_POINT ( 'NONE',  ( 4.084222279847079307, 13.38246373452060567, -136.0552959530092494 ) ) ;
#8798=PRESENTATION_STYLE_ASSIGNMENT (( #1577 ) ) ;
#8799=EDGE_CURVE ( 'NONE', #10448, #8129, #9300, .T. ) ;
#8800=CARTESIAN_POINT ( 'NONE',  ( -2.499999999969999998, 40.00000000000000000, -136.5552959530000123 ) ) ;
#8802=EDGE_CURVE ( 'NONE', #16549, #13712, #5410, .T. ) ;
#8814=ORIENTED_EDGE ( 'NONE', *, *, #21981, .T. ) ;
#8823=CARTESIAN_POINT ( 'NONE',  ( 7.930443943721122935, -30.97545875220255951, -136.0552959530179180 ) ) ;
#8825=CARTESIAN_POINT ( 'NONE',  ( 18.09818317350092798, 24.33939095841219213, -136.0552959530408543 ) ) ;
#8831=CARTESIAN_POINT ( 'NONE',  ( -7.102348325384737926, 25.50000000000001421, -136.0552959529839541 ) ) ;
#8836=DIRECTION ( 'NONE',  ( 1.000000000000000000, -5.094701932209999624E-24, 0.000000000000000000 ) ) ;
#8844=PRODUCT_CONTEXT ( 'NONE', #5834, 'mechanical' ) ;
#8856=CARTESIAN_POINT ( 'NONE',  ( 8.750000000030000891, -44.75000000000000000, -136.5552959530000123 ) ) ;
#8859=DIRECTION ( 'NONE',  ( 2.257749542879999954E-12, 0.000000000000000000, 1.000000000000000000 ) ) ;
#8865=DIRECTION ( 'NONE',  ( 5.094701932209999624E-24, 1.000000000000000000, 0.000000000000000000 ) ) ;
#8866=ORIENTED_EDGE ( 'NONE', *, *, #8925, .T. ) ;
#8872=FACE_OUTER_BOUND ( 'NONE', #16918, .T. ) ;
#8891=CARTESIAN_POINT ( 'NONE',  ( 13.13369214870000157, -51.50000000000000000, -136.0552959530000123 ) ) ;
#8892=DIRECTION ( 'NONE',  ( 2.255973186040000320E-12, 0.000000000000000000, 1.000000000000000000 ) ) ;
#8911=CARTESIAN_POINT ( 'NONE',  ( 31.50000000000000000, -40.03620104870000063, -136.0552959530000123 ) ) ;
#8912=CARTESIAN_POINT ( 'NONE',  ( 4.500000000009999113, -3.500000000000000000, -136.0552959530000123 ) ) ;
#8914=VECTOR ( 'NONE', #3977, 1000.000000000000000 ) ;
#8916=CARTESIAN_POINT ( 'NONE',  ( 3.611688725869999975E-11, 50.50000000000000000, -136.0552959530000123 ) ) ;
#8922=CARTESIAN_POINT ( 'NONE',  ( 3.000000000009999113, -3.301139731415996259, -136.0552959530067483 ) ) ;
#8925=EDGE_CURVE ( 'NONE', #18032, #13504, #1894, .T. ) ;
#8940=CARTESIAN_POINT ( 'NONE',  ( 17.88080765324347610, 24.01462304341578147, -136.0552959530404280 ) ) ;
#8945=CARTESIAN_POINT ( 'NONE',  ( -7.101996734191970972, 19.49999999999998579, -136.0552959529840393 ) ) ;
#8948=PLANE ( 'NONE',  #14439 ) ;
#8950=VECTOR ( 'NONE', #19185, 1000.000000000000000 ) ;
#8952=DIRECTION ( 'NONE',  ( -0.7071067811865463515, 0.7071067811865487940, 1.591319668629388887E-12 ) ) ;
#8958=CARTESIAN_POINT ( 'NONE',  ( -15.00000000000000000, -44.50000000000000000, -136.0552959530000123 ) ) ;
#8959=EDGE_CURVE ( 'NONE', #14486, #4356, #11770, .T. ) ;
#8963=CARTESIAN_POINT ( 'NONE',  ( -12.50000000000000000, 22.50000000000000000, -136.0552959530000123 ) ) ;
#8972=CARTESIAN_POINT ( 'NONE',  ( 13.76008370044074880, 22.44588062469307488, -136.0552959530310773 ) ) ;
#8973=ORIENTED_EDGE ( 'NONE', *, *, #19128, .F. ) ;
#8979=FACE_BOUND ( 'NONE', #14716, .T. ) ;
#9013=DIRECTION ( 'NONE',  ( -1.000000000000000000, 0.000000000000000000, 2.257120985840000117E-12 ) ) ;
#9021=CARTESIAN_POINT ( 'NONE',  ( 31.50000000000000000, -2.273736754430000208E-12, -136.0552959530000123 ) ) ;
#9026=CARTESIAN_POINT ( 'NONE',  ( -14.24256961507097863, -41.69005684777777532, -136.0552959529678390 ) ) ;
#9029=CARTESIAN_POINT ( 'NONE',  ( -13.86630785130000021, -2.273736754430000208E-12, -136.0552959530000123 ) ) ;
#9034=ADVANCED_FACE ( 'NONE', ( #18643 ), #16856, .F. ) ;
#9046=CARTESIAN_POINT ( 'NONE',  ( 9.724682038211440727, -33.25721777958510472, -136.0552959530218970 ) ) ;
#9054=CARTESIAN_POINT ( 'NONE',  ( -7.499999999959999997, 25.50000000000000000, -136.0552959530000123 ) ) ;
#9057=ORIENTED_EDGE ( 'NONE', *, *, #7628, .T. ) ;
#9060=AXIS2_PLACEMENT_3D ( 'NONE', #16209, #7155, #10825 ) ;
#9061=ORIENTED_EDGE ( 'NONE', *, *, #3076, .T. ) ;
#9069=CARTESIAN_POINT ( 'NONE',  ( 19.50000000000000000, 51.50000000000000000, -137.0552959530000123 ) ) ;
#9073=LINE ( 'NONE', #16246, #8914 ) ;
#9091=DIRECTION ( 'NONE',  ( 1.000000000000000000, 0.000000000000000000, -2.262079412673756451E-12 ) ) ;
#9098=FACE_BOUND ( 'NONE', #16325, .T. ) ;
#9131=CARTESIAN_POINT ( 'NONE',  ( 16.13369214859999801, -50.50000000000000000, -137.0552959530000123 ) ) ;
#9141=CARTESIAN_POINT ( 'NONE',  ( -0.009529796579482698038, 16.74243713058401184, -136.0552959529999555 ) ) ;
#9149=FACE_OUTER_BOUND ( 'NONE', #23504, .T. ) ;
#9151=EDGE_CURVE ( 'NONE', #17363, #7834, #11595, .T. ) ;
#9154=EDGE_CURVE ( 'NONE', #15193, #7436, #17183, .T. ) ;
#9155=VECTOR ( 'NONE', #5553, 1000.000000000000000 ) ;
#9175=CARTESIAN_POINT ( 'NONE',  ( 8.920566648597572978, -31.65725470906492589, -136.0552959530201633 ) ) ;
#9176=PLANE ( 'NONE',  #17811 ) ;
#9178=EDGE_CURVE ( 'NONE', #8634, #19021, #6373, .T. ) ;
#9204=AXIS2_PLACEMENT_3D ( 'NONE', #17276, #14179, #1342 ) ;
#9205=ORIENTED_EDGE ( 'NONE', *, *, #19869, .F. ) ;
#9212=CARTESIAN_POINT ( 'NONE',  ( 9.824773488100881025, 27.24096059670117853, -136.0552959530222097 ) ) ;
#9214=DIRECTION ( 'NONE',  ( -1.000000000000000000, 0.000000000000000000, 2.262368070660000099E-12 ) ) ;
#9218=PLANE ( 'NONE',  #14459 ) ;
#9220=EDGE_CURVE ( 'NONE', #3556, #15239, #9932, .T. ) ;
#9226=EDGE_CURVE ( 'NONE', #14839, #2120, #920, .T. ) ;
#9227=ADVANCED_FACE ( 'NONE', ( #15419 ), #22677, .T. ) ;
#9244=LINE ( 'NONE', #16511, #2657 ) ;
#9258=LINE ( 'NONE', #14975, #21271 ) ;
#9259=EDGE_LOOP ( 'NONE', ( #17354, #17394, #23534, #7709 ) ) ;
#9260=DIRECTION ( 'NONE',  ( 2.255973186040000320E-12, 0.000000000000000000, 1.000000000000000000 ) ) ;
#9268=DIRECTION ( 'NONE',  ( 2.257144641399999941E-12, -8.049635444003269754E-35, 1.000000000000000000 ) ) ;
#9276=ORIENTED_EDGE ( 'NONE', *, *, #8719, .F. ) ;
#9280=CARTESIAN_POINT ( 'NONE',  ( 13.13369214870000157, 51.50000000000000000, -136.0552959530000123 ) ) ;
#9296=DIRECTION ( 'NONE',  ( 2.257083409060000051E-12, 0.000000000000000000, 1.000000000000000000 ) ) ;
#9300=LINE ( 'NONE', #14571, #3378 ) ;
#9303=LINE ( 'NONE', #2196, #7062 ) ;
#9308=CARTESIAN_POINT ( 'NONE',  ( 3.000000000010000001, -3.500000000000000000, -136.0552959530000123 ) ) ;
#9309=ORIENTED_EDGE ( 'NONE', *, *, #18810, .T. ) ;
#9319=CARTESIAN_POINT ( 'NONE',  ( 25.11919234684406277, 34.98537695656359858, -136.0552959530567421 ) ) ;
#9327=LINE ( 'NONE', #7221, #17315 ) ;
#9334=CARTESIAN_POINT ( 'NONE',  ( 6.500000000030000002, 13.00000000000000000, -137.0552959530000123 ) ) ;
#9364=CARTESIAN_POINT ( 'NONE',  ( 3.611688725869999975E-11, 19.50000000000000000, -136.0552959530000123 ) ) ;
#9365=VECTOR ( 'NONE', #17783, 1000.000000000000000 ) ;
#9366=ORIENTED_EDGE ( 'NONE', *, *, #417, .F. ) ;
#9385=VECTOR ( 'NONE', #16671, 1000.000000000000000 ) ;
#9388=ADVANCED_FACE ( 'NONE', ( #11655 ), #18933, .F. ) ;
#9391=LINE ( 'NONE', #18699, #10043 ) ;
#9404=CARTESIAN_POINT ( 'NONE',  ( 4.500000000009999113, -5.000000000000000000, -136.5552959530000123 ) ) ;
#9418=CARTESIAN_POINT ( 'NONE',  ( 22.50000000000000000, 33.50000000000000000, -136.5552959530000123 ) ) ;
#9432=ORIENTED_EDGE ( 'NONE', *, *, #21916, .T. ) ;
#9446=ORIENTED_EDGE ( 'NONE', *, *, #20582, .F. ) ;
#9457=ORIENTED_EDGE ( 'NONE', *, *, #1643, .T. ) ;
#9462=APPLICATION_CONTEXT ( 'automotive_design' ) ;
#9466=EDGE_CURVE ( 'NONE', #10468, #12804, #22870, .T. ) ;
#9468=AXIS2_PLACEMENT_3D ( 'NONE', #8646, #4635, #6879 ) ;
#9477=CARTESIAN_POINT ( 'NONE',  ( -15.00000000000000000, -41.50000000000000000, -136.5552959530000123 ) ) ;
#9478=ORIENTED_EDGE ( 'NONE', *, *, #16103, .F. ) ;
#9481=FACE_OUTER_BOUND ( 'NONE', #22826, .T. ) ;
#9482=DIRECTION ( 'NONE',  ( 2.256861364460000137E-12, 0.000000000000000000, 1.000000000000000000 ) ) ;
#9483=ORIENTED_EDGE ( 'NONE', *, *, #6101, .F. ) ;
#9490=DIRECTION ( 'NONE',  ( 2.257749542879999954E-12, 0.000000000000000000, 1.000000000000000000 ) ) ;
#9505=ORIENTED_EDGE ( 'NONE', *, *, #1853, .F. ) ;
#9515=DIRECTION ( 'NONE',  ( 2.255973186040000320E-12, 0.000000000000000000, 1.000000000000000000 ) ) ;
#9523=CARTESIAN_POINT ( 'NONE',  ( -15.50000000000000000, 21.50000000000000000, -136.0552959530000123 ) ) ;
#9531=EDGE_CURVE ( 'NONE', #21987, #7133, #15480, .T. ) ;
#9552=EDGE_LOOP ( 'NONE', ( #20455, #10274, #5721, #6497 ) ) ;
#9577=ORIENTED_EDGE ( 'NONE', *, *, #16106, .T. ) ;
#9615=FACE_OUTER_BOUND ( 'NONE', #19384, .T. ) ;
#9622=CARTESIAN_POINT ( 'NONE',  ( -15.19886026855731842, -44.49999999999996447, -136.0552959529656789 ) ) ;
#9630=ORIENTED_EDGE ( 'NONE', *, *, #99, .T. ) ;
#9638=VECTOR ( 'NONE', #19562, 1000.000000000000000 ) ;
#9647=ORIENTED_EDGE ( 'NONE', *, *, #11511, .F. ) ;
#9656=DIRECTION ( 'NONE',  ( 5.094701932209999624E-24, 1.000000000000000000, 0.000000000000000000 ) ) ;
#9671=CARTESIAN_POINT ( 'NONE',  ( 31.50000000000000000, 32.96379895120000469, -137.0552959530000123 ) ) ;
#9672=FACE_OUTER_BOUND ( 'NONE', #22648, .T. ) ;
#9694=ORIENTED_EDGE ( 'NONE', *, *, #4374, .F. ) ;
#9699=LINE ( 'NONE', #13058, #17808 ) ;
#9714=LINE ( 'NONE', #16991, #17713 ) ;
#9720=VECTOR ( 'NONE', #10855, 1000.000000000000000 ) ;
#9727=CARTESIAN_POINT ( 'NONE',  ( 6.500000000030000002, 20.50000000000000000, -137.0552959530000123 ) ) ;
#9734=EDGE_CURVE ( 'NONE', #21227, #8089, #11630, .T. ) ;
#9735=ORIENTED_EDGE ( 'NONE', *, *, #19791, .F. ) ;
#9739=DIRECTION ( 'NONE',  ( 1.000000000000000000, 0.000000000000000000, -2.257120985840000117E-12 ) ) ;
#9748=CARTESIAN_POINT ( 'NONE',  ( 14.00000000000000000, 20.50000000000000000, -136.5552959530000123 ) ) ;
#9754=CARTESIAN_POINT ( 'NONE',  ( 6.000000000010000001, -3.500000000000000000, -136.0552959530000123 ) ) ;
#9755=LINE ( 'NONE', #1230, #23339 ) ;
#9756=ORIENTED_EDGE ( 'NONE', *, *, #20450, .F. ) ;
#9760=ORIENTED_EDGE ( 'NONE', *, *, #16317, .F. ) ;
#9780=LINE ( 'NONE', #13134, #19844 ) ;
#9793=ADVANCED_FACE ( 'NONE', ( #13082 ), #13317, .F. ) ;
#9800=AXIS2_PLACEMENT_3D ( 'NONE', #16006, #11079, #1277 ) ;
#9812=EDGE_CURVE ( 'NONE', #14599, #5119, #20488, .T. ) ;
#9828=ORIENTED_EDGE ( 'NONE', *, *, #20561, .F. ) ;
#9830=CARTESIAN_POINT ( 'NONE',  ( -12.50000000000000000, 45.50000000000000000, -136.0552959530000123 ) ) ;
#9836=CARTESIAN_POINT ( 'NONE',  ( 15.50000000000000000, 36.50000000000000000, -137.0552959530000123 ) ) ;
#9839=VECTOR ( 'NONE', #8660, 1000.000000000000000 ) ;
#9842=ORIENTED_EDGE ( 'NONE', *, *, #633, .F. ) ;
#9843=AXIS2_PLACEMENT_3D ( 'NONE', #2241, #18875, #18522 ) ;
#9845=CIRCLE ( 'NONE', #11745, 2.000000000000000000 ) ;
#9852=ORIENTED_EDGE ( 'NONE', *, *, #22160, .T. ) ;
#9868=DIRECTION ( 'NONE',  ( 2.257749542879999954E-12, 0.000000000000000000, 1.000000000000000000 ) ) ;
#9876=DIRECTION ( 'NONE',  ( -5.094701932209999624E-24, -1.000000000000000000, 1.149947916579999802E-35 ) ) ;
#9880=CIRCLE ( 'NONE', #12555, 1.500000000000001332 ) ;
#9899=ADVANCED_FACE ( 'NONE', ( #4865 ), #19389, .F. ) ;
#9904=PLANE ( 'NONE',  #15662 ) ;
#9907=ORIENTED_EDGE ( 'NONE', *, *, #10942, .F. ) ;
#9912=VERTEX_POINT ( 'NONE', #21060 ) ;
#9924=EDGE_CURVE ( 'NONE', #13504, #4170, #19508, .T. ) ;
#9932=LINE ( 'NONE', #12075, #2675 ) ;
#9958=DIRECTION ( 'NONE',  ( 1.000000000000000000, 0.000000000000000000, -2.257453483404485639E-12 ) ) ;
#9970=ORIENTED_EDGE ( 'NONE', *, *, #2853, .T. ) ;
#10003=FACE_OUTER_BOUND ( 'NONE', #10530, .T. ) ;
#10009=DIRECTION ( 'NONE',  ( 1.000000000000000000, 0.000000000000000000, -2.262368070660000099E-12 ) ) ;
#10024=CYLINDRICAL_SURFACE ( 'NONE', #6838, 7.500000000000005329 ) ;
#10029=VECTOR ( 'NONE', #2881, 1000.000000000000000 ) ;
#10033=PLANE ( 'NONE',  #1749 ) ;
#10043=VECTOR ( 'NONE', #9739, 1000.000000000000000 ) ;
#10044=CARTESIAN_POINT ( 'NONE',  ( -0.6175362654355562864, 22.91577772018733583, -136.0552959529986197 ) ) ;
#10054=ORIENTED_EDGE ( 'NONE', *, *, #11164, .F. ) ;
#10061=EDGE_CURVE ( 'NONE', #6635, #22142, #5097, .T. ) ;
#10074=EDGE_CURVE ( 'NONE', #10304, #12120, #21158, .T. ) ;
#10075=CARTESIAN_POINT ( 'NONE',  ( 8.750000000030000891, -37.98606797749999942, -136.5552959530000123 ) ) ;
#10082=AXIS2_PLACEMENT_3D ( 'NONE', #22555, #17309, #22789 ) ;
#10105=CARTESIAN_POINT ( 'NONE',  ( 14.71940181160194427, 39.42378041200770156, -136.0552959530332373 ) ) ;
#10112=LINE ( 'NONE', #15722, #12988 ) ;
#10114=DIRECTION ( 'NONE',  ( 1.000000000000000000, 0.000000000000000000, -2.257453483404485639E-12 ) ) ;
#10120=ORIENTED_EDGE ( 'NONE', *, *, #1643, .F. ) ;
#10121=DIRECTION ( 'NONE',  ( 1.000000000000000000, 0.000000000000000000, -2.257453483404484831E-12 ) ) ;
#10142=B_SPLINE_CURVE_WITH_KNOTS ( 'NONE', 3,
 ( #18378, #11452, #18733, #13242, #13014, #2089, #15152, #20516, #11210, #9308 ),
 .UNSPECIFIED., .F., .F.,
 ( 4, 2, 2, 2, 4 ),
 ( 0.000000000000000000, 0.2499999999999997224, 0.5000000000000000000, 0.7500000000000002220, 1.000000000000000000 ),
 .UNSPECIFIED. ) ;
#10170=EDGE_CURVE ( 'NONE', #16332, #2684, #6730, .T. ) ;
#10171=ORIENTED_EDGE ( 'NONE', *, *, #15122, .F. ) ;
#10177=LINE ( 'NONE', #19358, #17114 ) ;
#10181=VECTOR ( 'NONE', #3126, 1000.000000000000000 ) ;
#10189=DIRECTION ( 'NONE',  ( 2.257083409060000051E-12, 0.000000000000000000, 1.000000000000000000 ) ) ;
#10201=LINE ( 'NONE', #17921, #15728 ) ;
#10219=AXIS2_PLACEMENT_3D ( 'NONE', #17524, #11676, #22762 ) ;
#10235=DIRECTION ( 'NONE',  ( 2.259525899719999991E-12, 0.000000000000000000, 1.000000000000000000 ) ) ;
#10252=DIRECTION ( 'NONE',  ( 0.000000000000000000, 1.603797727360000188E-26, -1.000000000000000000 ) ) ;
#10274=ORIENTED_EDGE ( 'NONE', *, *, #14171, .F. ) ;
#10281=CARTESIAN_POINT ( 'NONE',  ( 8.351115582570084683, -45.97632467507357035, -136.0552959530188559 ) ) ;
#10285=LINE ( 'NONE', #12065, #9365 ) ;
#10286=CARTESIAN_POINT ( 'NONE',  ( -2.976504231241439591, 42.55205464666336468, -136.0552959530011776 ) ) ;
#10292=CARTESIAN_POINT ( 'NONE',  ( -0.7601318171273256930, 22.44600007524324781, -136.0552959529983070 ) ) ;
#10296=VECTOR ( 'NONE', #2421, 1000.000000000000000 ) ;
#10297=ORIENTED_EDGE ( 'NONE', *, *, #5415, .T. ) ;
#10304=VERTEX_POINT ( 'NONE', #17325 ) ;
#10320=ORIENTED_EDGE ( 'NONE', *, *, #633, .T. ) ;
#10341=ORIENTED_EDGE ( 'NONE', *, *, #4458, .F. ) ;
#10346=CARTESIAN_POINT ( 'NONE',  ( 13.98502865247636961, 39.11890206003843673, -136.0552959530315889 ) ) ;
#10352=DIRECTION ( 'NONE',  ( 0.000000000000000000, 1.000000000000000000, 0.000000000000000000 ) ) ;
#10355=EDGE_CURVE ( 'NONE', #1242, #11614, #9845, .T. ) ;
#10357=FACE_OUTER_BOUND ( 'NONE', #14441, .T. ) ;
#10358=LINE ( 'NONE', #15964, #2988 ) ;
#10373=ADVANCED_FACE ( 'NONE', ( #18281 ), #19830, .F. ) ;
#10376=ORIENTED_EDGE ( 'NONE', *, *, #19383, .T. ) ;
#10387=ADVANCED_FACE ( 'NONE', ( #10877 ), #23512, .F. ) ;
#10391=CARTESIAN_POINT ( 'NONE',  ( 5.004065293357752964, -45.75992235983020606, -136.0552959530113242 ) ) ;
#10393=AXIS2_PLACEMENT_3D ( 'NONE', #2738, #13427, #13666 ) ;
#10401=( LENGTH_UNIT ( ) NAMED_UNIT ( * ) SI_UNIT ( .MILLI., .METRE. ) );
#10409=CARTESIAN_POINT ( 'NONE',  ( 32.50000000000000000, 26.96379895119999759, -137.0552959530000123 ) ) ;
#10411=EDGE_CURVE ( 'NONE', #2271, #7733, #20014, .T. ) ;
#10435=EDGE_CURVE ( 'NONE', #19654, #19967, #13139, .T. ) ;
#10440=ORIENTED_EDGE ( 'NONE', *, *, #15196, .T. ) ;
#10444=CARTESIAN_POINT ( 'NONE',  ( 31.50000000000000000, 20.96379895120000114, -136.5552959530000123 ) ) ;
#10445=DIRECTION ( 'NONE',  ( 5.094701932209999624E-24, 1.000000000000000000, -1.149947916579999802E-35 ) ) ;
#10448=VERTEX_POINT ( 'NONE', #22305 ) ;
#10457=LINE ( 'NONE', #19641, #7646 ) ;
#10464=DIRECTION ( 'NONE',  ( 1.000000000000000000, 0.000000000000000000, -2.257120985840000117E-12 ) ) ;
#10468=VERTEX_POINT ( 'NONE', #9671 ) ;
#10481=CARTESIAN_POINT ( 'NONE',  ( 9.444192711154135722, -32.39608312526165435, -136.0552959530213002 ) ) ;
#10491=ORIENTED_EDGE ( 'NONE', *, *, #2860, .F. ) ;
#10497=CARTESIAN_POINT ( 'NONE',  ( 31.50000000010000178, -33.03620104880000241, -136.0552959530000123 ) ) ;
#10506=ORIENTED_EDGE ( 'NONE', *, *, #13645, .F. ) ;
#10514=LINE ( 'NONE', #17795, #3098 ) ;
#10523=DIRECTION ( 'NONE',  ( 1.000000000000000000, 0.000000000000000000, -2.257144641399999941E-12 ) ) ;
#10525=EDGE_CURVE ( 'NONE', #2277, #17363, #7888, .T. ) ;
#10530=EDGE_LOOP ( 'NONE', ( #1918, #3903, #5946, #13935 ) ) ;
#10551=ORIENTED_EDGE ( 'NONE', *, *, #7072, .F. ) ;
#10552=CARTESIAN_POINT ( 'NONE',  ( 23.50000000000000000, -20.50000000000000000, -137.0552959530000123 ) ) ;
#10553=AXIS2_PLACEMENT_3D ( 'NONE', #5772, #308, #1997 ) ;
#10564=ORIENTED_EDGE ( 'NONE', *, *, #907, .F. ) ;
#10576=VECTOR ( 'NONE', #18913, 1000.000000000000000 ) ;
#10587=DIRECTION ( 'NONE',  ( -2.257144641399999941E-12, 0.000000000000000000, -1.000000000000000000 ) ) ;
#10598=EDGE_CURVE ( 'NONE', #4637, #6536, #8361, .T. ) ;
#10600=DIRECTION ( 'NONE',  ( 2.257144641397284947E-12, -2.714760815920564689E-24, 1.000000000000000000 ) ) ;
#10607=FACE_OUTER_BOUND ( 'NONE', #795, .T. ) ;
#10608=DIRECTION ( 'NONE',  ( 2.259525899719999991E-12, 0.000000000000000000, 1.000000000000000000 ) ) ;
#10611=EDGE_CURVE ( 'NONE', #18787, #1242, #7962, .T. ) ;
#10621=ADVANCED_FACE ( 'NONE', ( #1142 ), #10024, .F. ) ;
#10627=VECTOR ( 'NONE', #22548, 1000.000000000000000 ) ;
#10635=ORIENTED_EDGE ( 'NONE', *, *, #13452, .F. ) ;
#10641=CARTESIAN_POINT ( 'NONE',  ( 24.90191174488025538, 38.33948587668919572, -136.0552959530562021 ) ) ;
#10644=DIRECTION ( 'NONE',  ( 0.000000000000000000, 1.000000000000000000, 0.000000000000000000 ) ) ;
#10661=AXIS2_PLACEMENT_3D ( 'NONE', #991, #880, #2889 ) ;
#10668=VERTEX_POINT ( 'NONE', #4574 ) ;
#10674=LINE ( 'NONE', #1671, #3051 ) ;
#10694=CARTESIAN_POINT ( 'NONE',  ( 19.13369214859999801, -50.50000000000000000, -136.5552959530000123 ) ) ;
#10697=VERTEX_POINT ( 'NONE', #3038 ) ;
#10701=CARTESIAN_POINT ( 'NONE',  ( 31.50000000000000000, 36.50000000000000000, -136.0552959530000123 ) ) ;
#10704=DIRECTION ( 'NONE',  ( 0.7071067811865469066, 0.7071067811865481278, -1.591319668629387474E-12 ) ) ;
#10710=EDGE_LOOP ( 'NONE', ( #8814, #9483, #16853, #8296 ) ) ;
#10711=MECHANICAL_DESIGN_GEOMETRIC_PRESENTATION_REPRESENTATION('',(#19841),#8444);
#10712=DIRECTION ( 'NONE',  ( 7.105427352510001232E-15, -1.000000000000000000, -1.603797727360000188E-26 ) ) ;
#10723=CARTESIAN_POINT ( 'NONE',  ( 3.906463970600278834, -34.75246044238718923, -136.0552959530088231 ) ) ;
#10727=ORIENTED_EDGE ( 'NONE', *, *, #5242, .F. ) ;
#10732=CIRCLE ( 'NONE', #7694, 1.499999999999999556 ) ;
#10738=DIRECTION ( 'NONE',  ( 5.094701932209999624E-24, 1.000000000000000000, -1.149947916579999802E-35 ) ) ;
#10743=LINE ( 'NONE', #12658, #18137 ) ;
#10751=VERTEX_POINT ( 'NONE', #15864 ) ;
#10755=CARTESIAN_POINT ( 'NONE',  ( 12.46241645107507168, 25.07592078381926015, -136.0552959530281214 ) ) ;
#10764=CARTESIAN_POINT ( 'NONE',  ( 8.463109132734597750, 13.19520492498762998, -136.0552959530044461 ) ) ;
#10766=ORIENTED_EDGE ( 'NONE', *, *, #19490, .F. ) ;
#10775=ORIENTED_EDGE ( 'NONE', *, *, #15787, .T. ) ;
#10791=ORIENTED_EDGE ( 'NONE', *, *, #16635, .F. ) ;
#10796=LINE ( 'NONE', #18200, #16541 ) ;
#10806=DIRECTION ( 'NONE',  ( 0.000000000000000000, 1.000000000000000000, 0.000000000000000000 ) ) ;
#10825=DIRECTION ( 'NONE',  ( 5.094701932209999624E-24, 1.000000000000000000, 0.000000000000000000 ) ) ;
#10839=CARTESIAN_POINT ( 'NONE',  ( 19.71940181160250560, 25.42378041200771221, -136.0552959530445207 ) ) ;
#10848=CARTESIAN_POINT ( 'NONE',  ( -4.499999999959999109, -2.273736754430000208E-12, -136.0552959530000123 ) ) ;
#10855=DIRECTION ( 'NONE',  ( 2.257157423930000049E-12, 0.000000000000000000, 1.000000000000000000 ) ) ;
#10869=EDGE_LOOP ( 'NONE', ( #444, #10120, #18030, #20468 ) ) ;
#10877=FACE_OUTER_BOUND ( 'NONE', #15194, .T. ) ;
#10882=FACE_BOUND ( 'NONE', #2961, .T. ) ;
#10896=ORIENTED_EDGE ( 'NONE', *, *, #8377, .T. ) ;
#10906=ORIENTED_EDGE ( 'NONE', *, *, #21107, .T. ) ;
#10908=CARTESIAN_POINT ( 'NONE',  ( -3.499999999969999998, 34.00000000000000000, -137.0552959530000123 ) ) ;
#10911=LINE ( 'NONE', #9131, #1112 ) ;
#10914=ORIENTED_EDGE ( 'NONE', *, *, #8617, .F. ) ;
#10921=CARTESIAN_POINT ( 'NONE',  ( 0.5375835489975798742, 15.92407921618114663, -136.0552959530012345 ) ) ;
#10922=EDGE_CURVE ( 'NONE', #6748, #20191, #10674, .T. ) ;
#10938=ORIENTED_EDGE ( 'NONE', *, *, #11697, .T. ) ;
#10940=CARTESIAN_POINT ( 'NONE',  ( 4.750000000030000002, -35.98606797749999942, -136.0552959530000123 ) ) ;
#10942=EDGE_CURVE ( 'NONE', #2120, #16131, #7121, .T. ) ;
#10957=CARTESIAN_POINT ( 'NONE',  ( 7.351088731987364788, -30.79529868152849303, -136.0552959530165822 ) ) ;
#10961=DIRECTION ( 'NONE',  ( 1.000000000000000000, 0.000000000000000000, -2.257453483404484831E-12 ) ) ;
#10965=CARTESIAN_POINT ( 'NONE',  ( -5.985376956567993290, 25.11919234682552116, -136.0552959529864552 ) ) ;
#10971=FACE_OUTER_BOUND ( 'NONE', #7058, .T. ) ;
#10976=EDGE_CURVE ( 'NONE', #9912, #11395, #21777, .T. ) ;
#10988=AXIS2_PLACEMENT_3D ( 'NONE', #9830, #15436, #4618 ) ;
#10999=DIRECTION ( 'NONE',  ( -0.7633862853691524286, 0.6459422414661292189, 0.000000000000000000 ) ) ;
#11013=VECTOR ( 'NONE', #11958, 1000.000000000000000 ) ;
#11019=CARTESIAN_POINT ( 'NONE',  ( 8.750000000030000891, -35.98606797749999942, -136.0552959530000123 ) ) ;
#11022=ORIENTED_EDGE ( 'NONE', *, *, #13645, .T. ) ;
#11027=AXIS2_PLACEMENT_3D ( 'NONE', #18792, #9268, #597 ) ;
#11037=ORIENTED_EDGE ( 'NONE', *, *, #4869, .T. ) ;
#11040=ORIENTED_EDGE ( 'NONE', *, *, #5300, .T. ) ;
#11046=VERTEX_POINT ( 'NONE', #22337 ) ;
#11055=CARTESIAN_POINT ( 'NONE',  ( 13.13369214870000157, 50.50000000000000000, -136.0552959530000123 ) ) ;
#11068=CARTESIAN_POINT ( 'NONE',  ( 4.890679856720475449, -2.038243779785305687, -136.0552959530110684 ) ) ;
#11073=VECTOR ( 'NONE', #10806, 1000.000000000000000 ) ;
#11079=DIRECTION ( 'NONE',  ( -5.094701932209999624E-24, -1.000000000000000000, 1.149947916579999802E-35 ) ) ;
#11096=CARTESIAN_POINT ( 'NONE',  ( -32.50000000000000000, 49.50000000000000000, -137.0552959530000123 ) ) ;
#11113=EDGE_CURVE ( 'NONE', #8089, #18676, #10177, .T. ) ;
#11115=CARTESIAN_POINT ( 'NONE',  ( 25.42349012529465924, 35.71905350742473928, -136.0552959530573673 ) ) ;
#11120=CARTESIAN_POINT ( 'NONE',  ( 12.49750131802634989, 15.89089960018812775, -136.0552959530134842 ) ) ;
#11128=DIRECTION ( 'NONE',  ( 2.257749542879999954E-12, 0.000000000000000000, 1.000000000000000000 ) ) ;
#11137=DIRECTION ( 'NONE',  ( 0.000000000000000000, 1.000000000000000000, 0.000000000000000000 ) ) ;
#11141=VECTOR ( 'NONE', #22543, 1000.000000000000000 ) ;
#11164=EDGE_CURVE ( 'NONE', #15695, #1359, #16488, .T. ) ;
#11168=ORIENTED_EDGE ( 'NONE', *, *, #1266, .F. ) ;
#11177=CARTESIAN_POINT ( 'NONE',  ( -16.20113092416073997, -43.92022845431750966, -136.0552959529634336 ) ) ;
#11184=ORIENTED_EDGE ( 'NONE', *, *, #1525, .T. ) ;
#11204=ORIENTED_EDGE ( 'NONE', *, *, #8066, .T. ) ;
#11206=CARTESIAN_POINT ( 'NONE',  ( 1.133692148650000009, -50.50000000000000000, -137.0552959530000123 ) ) ;
#11210=CARTESIAN_POINT ( 'NONE',  ( 3.000000000010000001, -3.699232232950709243, -136.0552959530068051 ) ) ;
#11212=ADVANCED_FACE ( 'NONE', ( #18046, #18162, #23518, #7437, #8979, #21968, #5654, #3405, #10882, #9098, #1757, #3291 ), #9218, .F. ) ;
#11214=ORIENTED_EDGE ( 'NONE', *, *, #4674, .F. ) ;
#11219=VECTOR ( 'NONE', #14573, 1000.000000000000000 ) ;
#11220=CARTESIAN_POINT ( 'NONE',  ( 10.25767361208684036, 27.00937110138498909, -136.0552959530231760 ) ) ;
#11224=FACE_OUTER_BOUND ( 'NONE', #23479, .T. ) ;
#11242=VERTEX_POINT ( 'NONE', #3533 ) ;
#11244=ORIENTED_EDGE ( 'NONE', *, *, #18983, .F. ) ;
#11248=ADVANCED_FACE ( 'NONE', ( #17929 ), #21860, .F. ) ;
#11249=PLANE ( 'NONE',  #9843 ) ;
#11260=EDGE_CURVE ( 'NONE', #17461, #4448, #12284, .T. ) ;
#11264=AXIS2_PLACEMENT_3D ( 'NONE', #2462, #3770, #435 ) ;
#11284=CARTESIAN_POINT ( 'NONE',  ( -5.449266527167752727, 43.97928331370520993, -136.0552959529877342 ) ) ;
#11295=B_SPLINE_CURVE_WITH_KNOTS ( 'NONE', 3,
 ( #697, #8922, #4144, #21692, #18106, #22464, #6160, #13410, #18228, #5377 ),
 .UNSPECIFIED., .F., .F.,
 ( 4, 2, 2, 2, 4 ),
 ( 0.000000000000000000, 0.2500000000000001110, 0.5000000000000002220, 0.7500000000000003331, 1.000000000000000000 ),
 .UNSPECIFIED. ) ;
#11310=ORIENTED_EDGE ( 'NONE', *, *, #11260, .F. ) ;
#11314=ORIENTED_EDGE ( 'NONE', *, *, #20251, .F. ) ;
#11315=LINE ( 'NONE', #18368, #4214 ) ;
#11342=CARTESIAN_POINT ( 'NONE',  ( 10.27714235282173938, 13.94660208734305940, -136.0552959530085388 ) ) ;
#11358=ORIENTED_EDGE ( 'NONE', *, *, #15208, .T. ) ;
#11372=VECTOR ( 'NONE', #1842, 1000.000000000000000 ) ;
#11389=CARTESIAN_POINT ( 'NONE',  ( -32.50000000000000000, 51.50000000000000000, -136.0552959530000123 ) ) ;
#11395=VERTEX_POINT ( 'NONE', #2685 ) ;
#11402=ORIENTED_EDGE ( 'NONE', *, *, #16399, .F. ) ;
#11406=CYLINDRICAL_SURFACE ( 'NONE', #18234, 2.000000000000001776 ) ;
#11409=LINE ( 'NONE', #11635, #10576 ) ;
#11414=VECTOR ( 'NONE', #88, 1000.000000000000000 ) ;
#11420=ORIENTED_EDGE ( 'NONE', *, *, #13176, .F. ) ;
#11425=CARTESIAN_POINT ( 'NONE',  ( 13.09818317349319017, 38.33939095840919720, -136.0552959530295709 ) ) ;
#11434=DIRECTION ( 'NONE',  ( 2.256861364460000137E-12, 0.000000000000000000, 1.000000000000000000 ) ) ;
#11452=CARTESIAN_POINT ( 'NONE',  ( 4.301139731426199653, -5.000000000000003553, -136.0552959530097041 ) ) ;
#11464=CARTESIAN_POINT ( 'NONE',  ( -9.999999999969999109, 48.50000000000000000, -137.0552959530000123 ) ) ;
#11469=FACE_BOUND ( 'NONE', #2573, .T. ) ;
#11480=ADVANCED_FACE ( 'NONE', ( #10971 ), #17898, .F. ) ;
#11496=CARTESIAN_POINT ( 'NONE',  ( -13.86630785130000021, -51.50000000000000000, -137.0552959530000123 ) ) ;
#11500=PLANE ( 'NONE',  #10988 ) ;
#11505=ORIENTED_EDGE ( 'NONE', *, *, #11113, .T. ) ;
#11511=EDGE_CURVE ( 'NONE', #21987, #3746, #17773, .T. ) ;
#11520=ORIENTED_EDGE ( 'NONE', *, *, #7514, .T. ) ;
#11530=DIRECTION ( 'NONE',  ( 5.094701932209999624E-24, 1.000000000000000000, 0.000000000000000000 ) ) ;
#11534=ADVANCED_FACE ( 'NONE', ( #7064 ), #14323, .F. ) ;
#11540=VECTOR ( 'NONE', #20999, 1000.000000000000000 ) ;
#11554=ORIENTED_EDGE ( 'NONE', *, *, #8235, .T. ) ;
#11566=ORIENTED_EDGE ( 'NONE', *, *, #5698, .T. ) ;
#11570=LINE ( 'NONE', #2556, #5747 ) ;
#11573=CARTESIAN_POINT ( 'NONE',  ( 25.49993271309264387, 36.89748944255538987, -136.0552959530575947 ) ) ;
#11575=CIRCLE ( 'NONE', #17677, 7.499999999999999112 ) ;
#11581=DIRECTION ( 'NONE',  ( 1.000000000000000000, -5.094701932209999624E-24, -2.257144641399999941E-12 ) ) ;
#11582=EDGE_CURVE ( 'NONE', #11841, #13781, #22285, .T. ) ;
#11592=ORIENTED_EDGE ( 'NONE', *, *, #4374, .T. ) ;
#11595=LINE ( 'NONE', #6725, #11013 ) ;
#11605=VERTEX_POINT ( 'NONE', #7521 ) ;
#11610=EDGE_CURVE ( 'NONE', #5331, #7124, #11315, .T. ) ;
#11614=VERTEX_POINT ( 'NONE', #20504 ) ;
#11616=CARTESIAN_POINT ( 'NONE',  ( 4.750000000030000002, -40.36803398869999882, -136.0552959530000123 ) ) ;
#11622=CARTESIAN_POINT ( 'NONE',  ( 22.50000000000000000, 36.50000000000000000, -136.0552959530000123 ) ) ;
#11630=LINE ( 'NONE', #14879, #14027 ) ;
#11635=CARTESIAN_POINT ( 'NONE',  ( 1.133692148650000009, -2.273736754430000208E-12, -136.0552959530000123 ) ) ;
#11638=VECTOR ( 'NONE', #15277, 1000.000000000000000 ) ;
#11654=VECTOR ( 'NONE', #262, 1000.000000000000000 ) ;
#11655=FACE_OUTER_BOUND ( 'NONE', #21380, .T. ) ;
#11676=DIRECTION ( 'NONE',  ( -5.094701932209999624E-24, -1.000000000000000000, 1.149947916579999802E-35 ) ) ;
#11683=VERTEX_POINT ( 'NONE', #11913 ) ;
#11696=ADVANCED_FACE ( 'NONE', ( #10003 ), #17514, .T. ) ;
#11697=EDGE_CURVE ( 'NONE', #20106, #6084, #22852, .T. ) ;
#11703=CIRCLE ( 'NONE', #23129, 2.000000000000000000 ) ;
#11715=CARTESIAN_POINT ( 'NONE',  ( -0.9999999999639999082, 20.50000000000000000, -136.0552959530000123 ) ) ;
#11727=CARTESIAN_POINT ( 'NONE',  ( -12.50000000000000000, 42.50000000000000000, -137.0552959530000123 ) ) ;
#11738=CARTESIAN_POINT ( 'NONE',  ( 8.750000000030000891, -42.36803398869999882, -137.0552959530000123 ) ) ;
#11745=AXIS2_PLACEMENT_3D ( 'NONE', #7326, #17797, #9091 ) ;
#11746=CARTESIAN_POINT ( 'NONE',  ( 22.50000000000000000, 39.50000000000000000, -136.0552959530000123 ) ) ;
#11747=ADVANCED_FACE ( 'NONE', ( #19315 ), #4688, .F. ) ;
#11764=AXIS2_PLACEMENT_3D ( 'NONE', #13764, #3061, #17917 ) ;
#11766=DIRECTION ( 'NONE',  ( -1.000000000000000000, 0.000000000000000000, 2.257120985840000117E-12 ) ) ;
#11770=B_SPLINE_CURVE_WITH_KNOTS ( 'NONE', 3,
 ( #20083, #14257, #23536, #19854, #16163, #3551, #15918, #3310, #3782, #17708 ),
 .UNSPECIFIED., .F., .F.,
 ( 4, 2, 2, 2, 4 ),
 ( 0.000000000000000000, 0.2500000000000000000, 0.5000000000000000000, 0.7500000000000000000, 1.000000000000000000 ),
 .UNSPECIFIED. ) ;
#11788=CARTESIAN_POINT ( 'NONE',  ( -32.50000000000000000, -51.50000000000000000, -137.0552959530000123 ) ) ;
#11806=ORIENTED_EDGE ( 'NONE', *, *, #10611, .T. ) ;
#11828=ORIENTED_EDGE ( 'NONE', *, *, #15787, .F. ) ;
#11831=VECTOR ( 'NONE', #396, 1000.000000000000000 ) ;
#11833=EDGE_CURVE ( 'NONE', #4825, #20191, #19079, .T. ) ;
#11839=CARTESIAN_POINT ( 'NONE',  ( 6.500000000040000003, 28.00000000000000000, -136.0552959530000123 ) ) ;
#11841=VERTEX_POINT ( 'NONE', #19910 ) ;
#11854=LINE ( 'NONE', #22690, #12505 ) ;
#11856=ORIENTED_EDGE ( 'NONE', *, *, #11833, .F. ) ;
#11857=EDGE_CURVE ( 'NONE', #11683, #1522, #21722, .T. ) ;
#11858=B_SPLINE_CURVE_WITH_KNOTS ( 'NONE', 3,
 ( #5713, #14881, #6069, #22141, #5826, #721, #4051, #11284, #492, #7727 ),
 .UNSPECIFIED., .F., .F.,
 ( 4, 2, 2, 2, 4 ),
 ( 0.000000000000000000, 0.2500000000000000000, 0.5000000000000000000, 0.7500000000000000000, 1.000000000000000000 ),
 .UNSPECIFIED. ) ;
#11882=ORIENTED_EDGE ( 'NONE', *, *, #13526, .T. ) ;
#11888=DIRECTION ( 'NONE',  ( -1.000000000000000000, 0.000000000000000000, 2.262368070660000099E-12 ) ) ;
#11891=DIRECTION ( 'NONE',  ( -1.000000000000000000, 5.094701932209999624E-24, 2.257144641399999941E-12 ) ) ;
#11900=DIRECTION ( 'NONE',  ( -5.094701932209999624E-24, -1.000000000000000000, 1.149947916579999802E-35 ) ) ;
#11913=CARTESIAN_POINT ( 'NONE',  ( 4.750000000030000002, -35.98606797749999942, -137.0552959530000123 ) ) ;
#11916=VERTEX_POINT ( 'NONE', #18245 ) ;
#11926=AXIS2_PLACEMENT_3D ( 'NONE', #13573, #13700, #10114 ) ;
#11936=VERTEX_POINT ( 'NONE', #2528 ) ;
#11938=VECTOR ( 'NONE', #12846, 1000.000000000000000 ) ;
#11945=EDGE_CURVE ( 'NONE', #6729, #14496, #624, .T. ) ;
#11947=B_SPLINE_CURVE_WITH_KNOTS ( 'NONE', 3,
 ( #18698, #14653, #11068, #2408, #149, #611, #379, #12853, #16550, #20137 ),
 .UNSPECIFIED., .F., .F.,
 ( 4, 2, 2, 2, 4 ),
 ( 0.000000000000000000, 0.2500000000000000000, 0.5000000000000000000, 0.7500000000000000000, 1.000000000000000000 ),
 .UNSPECIFIED. ) ;
#11958=DIRECTION ( 'NONE',  ( 1.000000000000000000, 0.000000000000000000, -2.257120985840000117E-12 ) ) ;
#11972=CARTESIAN_POINT ( 'NONE',  ( 19.13369214859999801, 50.50000000000000000, -136.0552959530000123 ) ) ;
#11979=CARTESIAN_POINT ( 'NONE',  ( 19.00000000000000000, 33.50000000000000000, -137.0552959530000123 ) ) ;
#11988=PRODUCT ( 'Cover Plate', 'Cover Plate', '', ( #8844 ) ) ;
#11991=ORIENTED_EDGE ( 'NONE', *, *, #10922, .T. ) ;
#12005=ADVANCED_FACE ( 'NONE', ( #6436 ), #20970, .T. ) ;
#12013=VECTOR ( 'NONE', #15656, 1000.000000000000000 ) ;
#12016=CARTESIAN_POINT ( 'NONE',  ( 8.250000000030000891, -39.98606797749999942, -137.0552959530000123 ) ) ;
#12027=ADVANCED_FACE ( 'NONE', ( #6668 ), #17382, .T. ) ;
#12028=CIRCLE ( 'NONE', #18124, 2.999999999999999112 ) ;
#12030=EDGE_LOOP ( 'NONE', ( #10791, #4970, #3282, #22640 ) ) ;
#12032=CYLINDRICAL_SURFACE ( 'NONE', #20881, 1.500000000000001110 ) ;
#12036=CARTESIAN_POINT ( 'NONE',  ( 8.750000000030000891, -37.98606797749999942, -136.0552959530000123 ) ) ;
#12048=ORIENTED_EDGE ( 'NONE', *, *, #4786, .T. ) ;
#12065=CARTESIAN_POINT ( 'NONE',  ( -3.499999999969999998, 46.50000000000000000, -136.5552959530000123 ) ) ;
#12075=CARTESIAN_POINT ( 'NONE',  ( 31.50000000000000000, 40.03620104880000241, -136.5552959530000123 ) ) ;
#12077=VERTEX_POINT ( 'NONE', #5014 ) ;
#12078=VERTEX_POINT ( 'NONE', #5234 ) ;
#12087=EDGE_LOOP ( 'NONE', ( #17822, #4906, #1930, #3775, #10297, #4855, #16815, #23483, #6013, #2487, #3469, #17381, #5780, #677, #21647, #8208, #4601, #559, #237, #22601, #11420, #7929, #14051, #9061, #18100, #3872, #9457, #12224, #19284, #1284, #9630, #5428 ) ) ;
#12100=ORIENTED_EDGE ( 'NONE', *, *, #11697, .F. ) ;
#12119=EDGE_CURVE ( 'NONE', #14496, #1756, #10457, .T. ) ;
#12120=VERTEX_POINT ( 'NONE', #8911 ) ;
#12122=VECTOR ( 'NONE', #1115, 1000.000000000000000 ) ;
#12129=AXIS2_PLACEMENT_3D ( 'NONE', #3399, #23394, #8616 ) ;
#12149=VECTOR ( 'NONE', #12251, 1000.000000000000000 ) ;
#12156=ADVANCED_FACE ( 'NONE', ( #9149 ), #19531, .T. ) ;
#12172=ORIENTED_EDGE ( 'NONE', *, *, #6903, .F. ) ;
#12179=MANIFOLD_SOLID_BREP ( 'lock_assembly.1\\lock body.2\\PartBody', #17147 ) ;
#12188=DIRECTION ( 'NONE',  ( -1.000000000000000000, 0.000000000000000000, 2.257120985840000117E-12 ) ) ;
#12189=CARTESIAN_POINT ( 'NONE',  ( 8.750000000030000891, -39.98606797749999942, -136.0552959530000123 ) ) ;
#12193=FACE_OUTER_BOUND ( 'NONE', #14699, .T. ) ;
#12195=ORIENTED_EDGE ( 'NONE', *, *, #19999, .F. ) ;
#12196=FILL_AREA_STYLE ('',( #15773 ) ) ;
#12202=VECTOR ( 'NONE', #16710, 1000.000000000000000 ) ;
#12224=ORIENTED_EDGE ( 'NONE', *, *, #10061, .T. ) ;
#12241=LINE ( 'NONE', #10444, #21936 ) ;
#12251=DIRECTION ( 'NONE',  ( 0.000000000000000000, 1.000000000000000000, 0.000000000000000000 ) ) ;
#12279=CYLINDRICAL_SURFACE ( 'NONE', #13588, 7.500000000000005329 ) ;
#12280=CARTESIAN_POINT ( 'NONE',  ( 8.750000000030000891, -35.98606797749999942, -136.0552959530000123 ) ) ;
#12284=B_SPLINE_CURVE_WITH_KNOTS ( 'NONE', 3,
 ( #1999, #5308, #10764, #11342, #20650, #11120, #16840, #18854, #18628, #2343 ),
 .UNSPECIFIED., .F., .F.,
 ( 4, 2, 2, 2, 4 ),
 ( 0.000000000000000000, 0.2500000000000000000, 0.5000000000000000000, 0.7500000000000000000, 1.000000000000000000 ),
 .UNSPECIFIED. ) ;
#12289=CARTESIAN_POINT ( 'NONE',  ( 32.50000000000000000, 32.96379895120000469, -137.0552959530000123 ) ) ;
#12293=LINE ( 'NONE', #10848, #11372 ) ;
#12300=CARTESIAN_POINT ( 'NONE',  ( 1.133692148650000009, 50.50000000000000000, -137.0552959530000123 ) ) ;
#12307=DIRECTION ( 'NONE',  ( -2.257144641399999941E-12, 8.049635416090000264E-35, -1.000000000000000000 ) ) ;
#12376=EDGE_CURVE ( 'NONE', #4637, #17721, #14467, .T. ) ;
#12377=VERTEX_POINT ( 'NONE', #23389 ) ;
#12378=B_SPLINE_CURVE_WITH_KNOTS ( 'NONE', 3,
 ( #12390, #15979, #12512, #19794, #10723, #21460, #14308, #7290, #5040, #18242, #21820, #23241, #3488, #1477, #18119, #3248, #14556, #19554, #10957, #8823, #18004, #5261, #9175, #158, #10481, #16451, #9046, #16100, #19666, #1715, #1954, #1830, #6935, #12280 ),
 .UNSPECIFIED., .F., .F.,
 ( 4, 2, 2, 2, 2, 2, 2, 2, 2, 2, 2, 2, 2, 2, 2, 2, 4 ),
 ( 0.000000000000000000, 0.06250000000000000000, 0.1250000000000000000, 0.1875000000000000000, 0.2500000000000000000, 0.3125000000000000000, 0.3750000000000000000, 0.4375000000000000000, 0.5000000000000000000, 0.5625000000000000000, 0.6250000000000000000, 0.6875000000000000000, 0.7500000000000000000, 0.8125000000000000000, 0.8750000000000000000, 0.9375000000000000000, 1.000000000000000000 ),
 .UNSPECIFIED. ) ;
#12380=VECTOR ( 'NONE', #15623, 1000.000000000000000 ) ;
#12382=ORIENTED_EDGE ( 'NONE', *, *, #21610, .F. ) ;
#12384=CARTESIAN_POINT ( 'NONE',  ( 23.00000000000000000, 19.50000000000000000, -136.0552959530000123 ) ) ;
#12389=FACE_OUTER_BOUND ( 'NONE', #2233, .T. ) ;
#12390=CARTESIAN_POINT ( 'NONE',  ( 4.750000000030000002, -35.98606797749999942, -136.0552959530000123 ) ) ;
#12392=CARTESIAN_POINT ( 'NONE',  ( 18.66060904169178869, 20.09818317339687255, -136.0552959530421333 ) ) ;
#12397=LINE ( 'NONE', #1482, #20606 ) ;
#12398=CARTESIAN_POINT ( 'NONE',  ( 31.50000000000000000, -0.03620104880649999829, -137.0552959530000123 ) ) ;
#12405=CARTESIAN_POINT ( 'NONE',  ( 3.611688725869999975E-11, -33.03620104880000241, -136.0552959530000123 ) ) ;
#12407=CARTESIAN_POINT ( 'NONE',  ( 5.148789539651774660, -45.97641955294970018, -136.0552959530116084 ) ) ;
#12427=ADVANCED_FACE ( 'NONE', ( #2334 ), #9904, .T. ) ;
#12429=ORIENTED_EDGE ( 'NONE', *, *, #11260, .T. ) ;
#12443=AXIS2_PLACEMENT_3D ( 'NONE', #19665, #3360, #7046 ) ;
#12449=CARTESIAN_POINT ( 'NONE',  ( -25.86630785129999666, -51.50000000000000000, -137.0552959530000123 ) ) ;
#12450=B_SPLINE_CURVE_WITH_KNOTS ( 'NONE', 3,
 ( #12476, #1570, #16303, #19634, #8787, #16065, #18204, #23323, #7014, #3688, #10921, #9141, #16421, #1683, #14277, #21546, #5227, #4036 ),
 .UNSPECIFIED., .F., .F.,
 ( 4, 2, 2, 2, 2, 2, 2, 2, 4 ),
 ( 0.000000000000000000, 0.1250000000000000000, 0.2500000000000000000, 0.3750000000000000000, 0.5000000000000000000, 0.6250000000000000000, 0.7500000000000000000, 0.8750000000000000000, 1.000000000000000000 ),
 .UNSPECIFIED. ) ;
#12467=ORIENTED_EDGE ( 'NONE', *, *, #5720, .T. ) ;
#12476=CARTESIAN_POINT ( 'NONE',  ( 6.500000000040000003, 13.00000000000000000, -136.0552959530000123 ) ) ;
#12480=CARTESIAN_POINT ( 'NONE',  ( 31.50000000010000178, -40.03620104880000241, -137.0552959530000123 ) ) ;
#12493=CARTESIAN_POINT ( 'NONE',  ( -15.00000000000000000, -43.00000000000000000, -136.0552959530000123 ) ) ;
#12494=ORIENTED_EDGE ( 'NONE', *, *, #14460, .F. ) ;
#12505=VECTOR ( 'NONE', #4264, 1000.000000000000000 ) ;
#12512=CARTESIAN_POINT ( 'NONE',  ( 4.332174032671896491, -35.55157851246247702, -136.0552959530098178 ) ) ;
#12515=ADVANCED_FACE ( 'NONE', ( #10607 ), #16563, .F. ) ;
#12522=CARTESIAN_POINT ( 'NONE',  ( -6.719401811520419265, 19.57621958799322570, -136.0552959529848351 ) ) ;
#12528=CARTESIAN_POINT ( 'NONE',  ( -15.00000000000000000, -43.00000000000000000, -136.0552959530000123 ) ) ;
#12529=CARTESIAN_POINT ( 'NONE',  ( 3.611688725869999975E-11, -21.03620104879999886, -136.0552959530000123 ) ) ;
#12537=CARTESIAN_POINT ( 'NONE',  ( 15.50000000000000000, 39.50000000000000000, -137.0552959530000123 ) ) ;
#12555=AXIS2_PLACEMENT_3D ( 'NONE', #2503, #20583, #7488 ) ;
#12556=ORIENTED_EDGE ( 'NONE', *, *, #6506, .F. ) ;
#12558=CARTESIAN_POINT ( 'NONE',  ( 3.385736135899999992E-11, -2.273736754430000208E-12, -137.0552959530000123 ) ) ;
#12572=CARTESIAN_POINT ( 'NONE',  ( -4.499999999969999109, 40.00000000000000000, -137.0552959530000123 ) ) ;
#12585=CARTESIAN_POINT ( 'NONE',  ( 1.133692148650000009, -50.50000000000000000, -136.5552959530000123 ) ) ;
#12618=CARTESIAN_POINT ( 'NONE',  ( -13.68932041746861294, -43.75542847055635320, -136.0552959530029682 ) ) ;
#12639=CARTESIAN_POINT ( 'NONE',  ( 17.57650987483295069, 23.28094649262697402, -136.0552959530396606 ) ) ;
#12649=ORIENTED_EDGE ( 'NONE', *, *, #21107, .F. ) ;
#12657=FACE_OUTER_BOUND ( 'NONE', #22676, .T. ) ;
#12658=CARTESIAN_POINT ( 'NONE',  ( 3.611688725869999975E-11, 32.96379895120000469, -136.0552959530000123 ) ) ;
#12672=CARTESIAN_POINT ( 'NONE',  ( 6.992624432290238445, 28.00000000000003553, -136.0552959530157864 ) ) ;
#12678=EDGE_LOOP ( 'NONE', ( #5091, #6351, #14070, #22361 ) ) ;
#12684=CARTESIAN_POINT ( 'NONE',  ( 22.50000000000000000, 36.50000000000000000, -137.0552959530000123 ) ) ;
#12703=ORIENTED_EDGE ( 'NONE', *, *, #1878, .T. ) ;
#12710=DIRECTION ( 'NONE',  ( -1.000000000000000000, 5.094701932209999624E-24, 2.257144641399999941E-12 ) ) ;
#12716=DIRECTION ( 'NONE',  ( 1.000000000000000000, 0.000000000000000000, -2.257120985840000117E-12 ) ) ;
#12727=CARTESIAN_POINT ( 'NONE',  ( -13.50000000000000000, -43.00000000000000000, -136.0552959530000123 ) ) ;
#12729=EDGE_CURVE ( 'NONE', #3746, #2000, #10112, .T. ) ;
#12737=AXIS2_PLACEMENT_3D ( 'NONE', #1644, #16143, #8865 ) ;
#12738=CARTESIAN_POINT ( 'NONE',  ( 13.13369214870000157, 51.00000000000000000, -137.0552959530000123 ) ) ;
#12744=CARTESIAN_POINT ( 'NONE',  ( -12.50000000000000000, 42.50000000000000000, -136.0552959530000123 ) ) ;
#12746=ORIENTED_EDGE ( 'NONE', *, *, #5698, .F. ) ;
#12752=DIRECTION ( 'NONE',  ( 1.000000000000000000, -5.094701932209999624E-24, 0.000000000000000000 ) ) ;
#12763=VECTOR ( 'NONE', #23491, 1000.000000000000000 ) ;
#12764=ORIENTED_EDGE ( 'NONE', *, *, #20551, .F. ) ;
#12786=CARTESIAN_POINT ( 'NONE',  ( 11.07581004124147483, 26.46257514628838692, -136.0552959530250234 ) ) ;
#12790=DIRECTION ( 'NONE',  ( 0.000000000000000000, 1.000000000000000000, 0.000000000000000000 ) ) ;
#12804=VERTEX_POINT ( 'NONE', #22871 ) ;
#12815=CARTESIAN_POINT ( 'NONE',  ( 31.50000000000000000, -40.03620104870000063, -136.0552959530000123 ) ) ;
#12833=EDGE_LOOP ( 'NONE', ( #11402, #22726, #14512, #493 ) ) ;
#12846=DIRECTION ( 'NONE',  ( 0.000000000000000000, 1.000000000000000000, 0.000000000000000000 ) ) ;
#12850=DIRECTION ( 'NONE',  ( 0.000000000000000000, 1.000000000000000000, 0.000000000000000000 ) ) ;
#12853=CARTESIAN_POINT ( 'NONE',  ( 5.961949895415374456, -3.109416060109817970, -136.0552959530134842 ) ) ;
#12855=EDGE_CURVE ( 'NONE', #15273, #8129, #3002, .T. ) ;
#12875=VECTOR ( 'NONE', #226, 1000.000000000000000 ) ;
#12888=B_SPLINE_CURVE_WITH_KNOTS ( 'NONE', 3,
 ( #17784, #13864, #10286, #23264, #21373, #6956, #19337, #3385, #7076, #14221 ),
 .UNSPECIFIED., .F., .F.,
 ( 4, 2, 2, 2, 4 ),
 ( 0.000000000000000000, 0.2500000000000000555, 0.5000000000000001110, 0.7500000000000000000, 1.000000000000000000 ),
 .UNSPECIFIED. ) ;
#12891=DIRECTION ( 'NONE',  ( -1.000000000000000000, 0.000000000000000000, 2.257120985840000117E-12 ) ) ;
#12892=CARTESIAN_POINT ( 'NONE',  ( -15.00000000000000000, -44.50000000000000000, -137.0552959530000123 ) ) ;
#12894=AXIS2_PLACEMENT_3D ( 'NONE', #3475, #10712, #10252 ) ;
#12901=ORIENTED_EDGE ( 'NONE', *, *, #12376, .F. ) ;
#12905=ORIENTED_EDGE ( 'NONE', *, *, #5874, .T. ) ;
#12915=DIRECTION ( 'NONE',  ( 1.000000000000000000, 0.000000000000000000, -2.257453483404485639E-12 ) ) ;
#12924=ORIENTED_EDGE ( 'NONE', *, *, #8382, .F. ) ;
#12934=ORIENTED_EDGE ( 'NONE', *, *, #9178, .T. ) ;
#12945=FACE_OUTER_BOUND ( 'NONE', #7455, .T. ) ;
#12948=VERTEX_POINT ( 'NONE', #20471 ) ;
#12949=AXIS2_PLACEMENT_3D ( 'NONE', #21352, #1131, #8362 ) ;
#12986=VECTOR ( 'NONE', #11434, 1000.000000000000000 ) ;
#12988=VECTOR ( 'NONE', #10352, 1000.000000000000000 ) ;
#13010=LINE ( 'NONE', #11096, #12763 ) ;
#13014=CARTESIAN_POINT ( 'NONE',  ( 3.579871919197813224, -4.701030550647564255, -136.0552959530081125 ) ) ;
#13016=EDGE_LOOP ( 'NONE', ( #21397, #19986, #11314, #8143 ) ) ;
#13052=ORIENTED_EDGE ( 'NONE', *, *, #10074, .F. ) ;
#13058=CARTESIAN_POINT ( 'NONE',  ( -19.86630785130000021, -51.50000000000000000, -137.0552959530000123 ) ) ;
#13067=VECTOR ( 'NONE', #873, 1000.000000000000000 ) ;
#13082=FACE_OUTER_BOUND ( 'NONE', #6344, .T. ) ;
#13102=VECTOR ( 'NONE', #9013, 1000.000000000000000 ) ;
#13134=CARTESIAN_POINT ( 'NONE',  ( -4.499999999969999109, 37.00000000000000000, -137.0552959530000123 ) ) ;
#13138=ORIENTED_EDGE ( 'NONE', *, *, #11833, .T. ) ;
#13139=LINE ( 'NONE', #11464, #15180 ) ;
#13145=AXIS2_PLACEMENT_3D ( 'NONE', #13809, #15707, #4759 ) ;
#13158=EDGE_CURVE ( 'NONE', #19654, #23517, #8537, .T. ) ;
#13176=EDGE_CURVE ( 'NONE', #7834, #10448, #17603, .T. ) ;
#13185=ORIENTED_EDGE ( 'NONE', *, *, #20450, .T. ) ;
#13193=CYLINDRICAL_SURFACE ( 'NONE', #11027, 2.999999999999999112 ) ;
#13202=CARTESIAN_POINT ( 'NONE',  ( -3.234790887152434458, 46.50000000000001421, -136.0552959529926795 ) ) ;
#13206=EDGE_CURVE ( 'NONE', #18341, #3836, #17356, .T. ) ;
#13215=CARTESIAN_POINT ( 'NONE',  ( 12.49993271309136311, 36.89748944249159024, -136.0552959530282635 ) ) ;
#13231=CARTESIAN_POINT ( 'NONE',  ( 4.750000000030000002, -44.75000000000000000, -136.5552959530000123 ) ) ;
#13234=EDGE_CURVE ( 'NONE', #15683, #22142, #7001, .T. ) ;
#13242=CARTESIAN_POINT ( 'NONE',  ( 3.742569615074119671, -4.809943152218662199, -136.0552959530084536 ) ) ;
#13267=VERTEX_POINT ( 'NONE', #3672 ) ;
#13269=ORIENTED_EDGE ( 'NONE', *, *, #5315, .T. ) ;
#13270=LINE ( 'NONE', #1031, #14151 ) ;
#13300=DIRECTION ( 'NONE',  ( -2.257144641399999941E-12, 8.049635416090000264E-35, -1.000000000000000000 ) ) ;
#13312=ORIENTED_EDGE ( 'NONE', *, *, #14297, .T. ) ;
#13317=CYLINDRICAL_SURFACE ( 'NONE', #4139, 2.000000000000001776 ) ;
#13335=CARTESIAN_POINT ( 'NONE',  ( 3.611688725869999975E-11, -39.98606797749999942, -136.0552959530000123 ) ) ;
#13345=LINE ( 'NONE', #3962, #21362 ) ;
#13350=CARTESIAN_POINT ( 'NONE',  ( 25.50000000000000000, 25.50000000000000000, -136.5552959530000123 ) ) ;
#13358=ORIENTED_EDGE ( 'NONE', *, *, #2305, .T. ) ;
#13361=DIRECTION ( 'NONE',  ( 2.259525899719999991E-12, 0.000000000000000000, 1.000000000000000000 ) ) ;
#13379=LINE ( 'NONE', #305, #7595 ) ;
#13384=DIRECTION ( 'NONE',  ( 2.257144641399999941E-12, -8.049635416090000264E-35, 1.000000000000000000 ) ) ;
#13401=LINE ( 'NONE', #8038, #3151 ) ;
#13410=CARTESIAN_POINT ( 'NONE',  ( 4.109416060118438629, -2.038050104594628653, -136.0552959530093062 ) ) ;
#13420=CARTESIAN_POINT ( 'NONE',  ( 4.500000000009999113, -3.500000000000000000, -137.0552959530000123 ) ) ;
#13422=ORIENTED_EDGE ( 'NONE', *, *, #16103, .T. ) ;
#13427=DIRECTION ( 'NONE',  ( -5.094701932209999624E-24, -1.000000000000000000, 1.149947916579999802E-35 ) ) ;
#13439=ORIENTED_EDGE ( 'NONE', *, *, #7628, .F. ) ;
#13452=EDGE_CURVE ( 'NONE', #8634, #20086, #3791, .T. ) ;
#13463=CARTESIAN_POINT ( 'NONE',  ( 32.50000000000000000, -21.03620104879999886, -137.0552959530000123 ) ) ;
#13465=EDGE_LOOP ( 'NONE', ( #10766, #18853, #9205, #18763 ) ) ;
#13469=ORIENTED_EDGE ( 'NONE', *, *, #19383, .F. ) ;
#13473=LINE ( 'NONE', #3021, #6798 ) ;
#13504=VERTEX_POINT ( 'NONE', #15424 ) ;
#13522=VECTOR ( 'NONE', #5031, 1000.000000000000000 ) ;
#13526=EDGE_CURVE ( 'NONE', #7124, #18273, #13401, .T. ) ;
#13542=CARTESIAN_POINT ( 'NONE',  ( -32.50000000000000000, 21.50000000000000000, -137.0552959530000123 ) ) ;
#13545=CARTESIAN_POINT ( 'NONE',  ( -7.499999999969999109, 48.50000000000000000, -136.5552959530000123 ) ) ;
#13573=CARTESIAN_POINT ( 'NONE',  ( 4.500000000009999113, -3.500000000000000000, -137.0552959530000123 ) ) ;
#13588=AXIS2_PLACEMENT_3D ( 'NONE', #3247, #10600, #23356 ) ;
#13590=ADVANCED_FACE ( 'NONE', ( #4544 ), #2536, .F. ) ;
#13595=CARTESIAN_POINT ( 'NONE',  ( 7.750000000030000002, -39.98606797749999942, -136.0552959530000123 ) ) ;
#13615=FACE_BOUND ( 'NONE', #5423, .T. ) ;
#13617=PLANE ( 'NONE',  #4027 ) ;
#13619=CARTESIAN_POINT ( 'NONE',  ( 6.500000000030000002, 20.50000000000000000, -137.0552959530000123 ) ) ;
#13626=CARTESIAN_POINT ( 'NONE',  ( -7.499999999959999997, 48.50000000000000000, -136.0552959530000123 ) ) ;
#13628=VECTOR ( 'NONE', #2854, 1000.000000000000000 ) ;
#13642=EDGE_LOOP ( 'NONE', ( #5531, #12556, #1311, #22100 ) ) ;
#13645=EDGE_CURVE ( 'NONE', #7133, #2000, #17034, .T. ) ;
#13654=DIRECTION ( 'NONE',  ( -2.257144641399999941E-12, 8.049635416090000264E-35, -1.000000000000000000 ) ) ;
#13666=DIRECTION ( 'NONE',  ( -1.000000000000000000, 5.094701932209999624E-24, 0.000000000000000000 ) ) ;
#13678=ORIENTED_EDGE ( 'NONE', *, *, #12119, .T. ) ;
#13689=CARTESIAN_POINT ( 'NONE',  ( -16.50000000000000000, -43.00000000000000000, -136.0552959530000123 ) ) ;
#13697=CARTESIAN_POINT ( 'NONE',  ( 31.50000000000000000, 32.96379895120000469, -136.5552959530000123 ) ) ;
#13700=DIRECTION ( 'NONE',  ( 2.257144641399999941E-12, -8.049635416090000264E-35, 1.000000000000000000 ) ) ;
#13703=ORIENTED_EDGE ( 'NONE', *, *, #1239, .T. ) ;
#13707=EDGE_CURVE ( 'NONE', #19082, #18664, #10732, .T. ) ;
#13712=VERTEX_POINT ( 'NONE', #13463 ) ;
#13732=CARTESIAN_POINT ( 'NONE',  ( -12.50000000000000000, 25.50000000000000000, -136.5552959530000123 ) ) ;
#13735=DIRECTION ( 'NONE',  ( 2.257144641397284947E-12, 2.714760815920564689E-24, 1.000000000000000000 ) ) ;
#13748=DIRECTION ( 'NONE',  ( -1.000000000000000000, 5.094701932209999624E-24, 2.257144641399999941E-12 ) ) ;
#13764=CARTESIAN_POINT ( 'NONE',  ( 1.133692148650000009, -51.00000000000000000, -136.0552959530000123 ) ) ;
#13778=VECTOR ( 'NONE', #2849, 1000.000000000000000 ) ;
#13780=FACE_OUTER_BOUND ( 'NONE', #10869, .T. ) ;
#13781=VERTEX_POINT ( 'NONE', #20979 ) ;
#13787=ORIENTED_EDGE ( 'NONE', *, *, #16736, .T. ) ;
#13789=DIRECTION ( 'NONE',  ( 2.257144641399999941E-12, -8.049635444003269754E-35, 1.000000000000000000 ) ) ;
#13792=ADVANCED_FACE ( 'NONE', ( #6445 ), #15613, .F. ) ;
#13800=DIRECTION ( 'NONE',  ( 0.000000000000000000, 1.000000000000000000, 0.000000000000000000 ) ) ;
#13801=ORIENTED_EDGE ( 'NONE', *, *, #4226, .F. ) ;
#13809=CARTESIAN_POINT ( 'NONE',  ( -3.499999999959999997, 44.50000000000000000, -136.0552959530000123 ) ) ;
#13810=LINE ( 'NONE', #21073, #15775 ) ;
#13812=DIRECTION ( 'NONE',  ( 5.094701932209999624E-24, 1.000000000000000000, -1.149947916579999802E-35 ) ) ;
#13820=DIRECTION ( 'NONE',  ( 1.000000000000000000, 0.000000000000000000, -2.262079412673756451E-12 ) ) ;
#13846=ADVANCED_FACE ( 'NONE', ( #10357 ), #6916, .F. ) ;
#13851=LINE ( 'NONE', #13732, #11540 ) ;
#13859=FACE_BOUND ( 'NONE', #8178, .T. ) ;
#13864=CARTESIAN_POINT ( 'NONE',  ( -3.238200612160851755, 42.50000000000000711, -136.0552959530006092 ) ) ;
#13868=ORIENTED_EDGE ( 'NONE', *, *, #10525, .F. ) ;
#13875=VERTEX_POINT ( 'NONE', #19297 ) ;
#13877=EDGE_CURVE ( 'NONE', #15726, #10697, #17511, .T. ) ;
#13891=ORIENTED_EDGE ( 'NONE', *, *, #13158, .T. ) ;
#13900=ORIENTED_EDGE ( 'NONE', *, *, #18983, .T. ) ;
#13918=LINE ( 'NONE', #22855, #7415 ) ;
#13935=ORIENTED_EDGE ( 'NONE', *, *, #16426, .F. ) ;
#13944=EDGE_LOOP ( 'NONE', ( #4048, #5904, #16921, #20580, #137, #17749, #16963, #6043 ) ) ;
#13946=LINE ( 'NONE', #6927, #20759 ) ;
#13948=PLANE ( 'NONE',  #10219 ) ;
#13952=AXIS2_PLACEMENT_3D ( 'NONE', #666, #22205, #7556 ) ;
#13964=ORIENTED_EDGE ( 'NONE', *, *, #22165, .F. ) ;
#13967=ORIENTED_EDGE ( 'NONE', *, *, #22617, .F. ) ;
#13986=CARTESIAN_POINT ( 'NONE',  ( 0.8488726857078380261, 25.45511797032530765, -136.0552959530019450 ) ) ;
#14000=CARTESIAN_POINT ( 'NONE',  ( 5.699500263607268913, -4.421820079962375694, -136.0552959530027124 ) ) ;
#14003=ORIENTED_EDGE ( 'NONE', *, *, #21981, .F. ) ;
#14007=DIRECTION ( 'NONE',  ( 0.000000000000000000, 1.000000000000000000, 0.000000000000000000 ) ) ;
#14020=ADVANCED_FACE ( 'NONE', ( #18101 ), #23340, .T. ) ;
#14027=VECTOR ( 'NONE', #15233, 1000.000000000000227 ) ;
#14043=ADVANCED_FACE ( 'NONE', ( #5373 ), #19893, .F. ) ;
#14046=LINE ( 'NONE', #5230, #7886 ) ;
#14048=AXIS2_PLACEMENT_3D ( 'NONE', #13420, #8291, #706 ) ;
#14051=ORIENTED_EDGE ( 'NONE', *, *, #2860, .T. ) ;
#14054=DIRECTION ( 'NONE',  ( 0.000000000000000000, 1.000000000000000000, 0.000000000000000000 ) ) ;
#14063=EDGE_LOOP ( 'NONE', ( #13900, #19970, #6751, #11806 ) ) ;
#14067=CIRCLE ( 'NONE', #15205, 1.500000000000001332 ) ;
#14070=ORIENTED_EDGE ( 'NONE', *, *, #13234, .F. ) ;
#14078=CARTESIAN_POINT ( 'NONE',  ( -0.9999999999660000860, 20.50000000000000000, -137.0552959530000123 ) ) ;
#14097=CARTESIAN_POINT ( 'NONE',  ( 6.229273316152252882, -46.69892946173250436, -136.0552959530140811 ) ) ;
#14098=AXIS2_PLACEMENT_3D ( 'NONE', #14311, #21708, #10961 ) ;
#14109=EDGE_LOOP ( 'NONE', ( #1353, #4714, #7342, #4535 ) ) ;
#14116=COLOUR_RGB ( '', 0.08235294, 0.09019608, 0.10196078) ;
#14133=LINE ( 'NONE', #17818, #15627 ) ;
#14137=ORIENTED_EDGE ( 'NONE', *, *, #1266, .T. ) ;
#14138=DIRECTION ( 'NONE',  ( 2.259525899719999991E-12, 0.000000000000000000, 1.000000000000000000 ) ) ;
#14151=VECTOR ( 'NONE', #2579, 1000.000000000000000 ) ;
#14168=DIRECTION ( 'NONE',  ( -1.000000000000000000, 0.000000000000000000, 2.257120985840000117E-12 ) ) ;
#14171=EDGE_CURVE ( 'NONE', #13781, #416, #11409, .T. ) ;
#14173=DIRECTION ( 'NONE',  ( 0.000000000000000000, -1.000000000000000000, 0.000000000000000000 ) ) ;
#14179=DIRECTION ( 'NONE',  ( 2.257144641399999941E-12, -8.049635416090000264E-35, 1.000000000000000000 ) ) ;
#14195=CYLINDRICAL_SURFACE ( 'NONE', #12443, 3.000000000000000000 ) ;
#14200=CARTESIAN_POINT ( 'NONE',  ( 20.10234832544897543, 19.49999999999997513, -136.0552959530453450 ) ) ;
#14203=ORIENTED_EDGE ( 'NONE', *, *, #11610, .T. ) ;
#14207=EDGE_LOOP ( 'NONE', ( #3714, #15373, #22231, #1253 ) ) ;
#14210=ORIENTED_EDGE ( 'NONE', *, *, #17684, .F. ) ;
#14216=CIRCLE ( 'NONE', #3211, 1.499999999999999556 ) ;
#14221=CARTESIAN_POINT ( 'NONE',  ( -1.499999999960000219, 44.50000000000000000, -136.0552959530000123 ) ) ;
#14224=ORIENTED_EDGE ( 'NONE', *, *, #23082, .F. ) ;
#14226=UNCERTAINTY_MEASURE_WITH_UNIT (LENGTH_MEASURE( 1.000000000000000082E-05 ), #23332, 'distance_accuracy_value', 'NONE');
#14228=( LENGTH_UNIT ( ) NAMED_UNIT ( * ) SI_UNIT ( .MILLI., .METRE. ) );
#14236=CARTESIAN_POINT ( 'NONE',  ( 23.28094649259046989, 39.42349012525005492, -136.0552959530525641 ) ) ;
#14255=ORIENTED_EDGE ( 'NONE', *, *, #16811, .F. ) ;
#14257=CARTESIAN_POINT ( 'NONE',  ( -5.499999999960006214, 44.76520911280675818, -136.0552959529875920 ) ) ;
#14262=DIRECTION ( 'NONE',  ( 2.257083409060000051E-12, 0.000000000000000000, 1.000000000000000000 ) ) ;
#14268=AXIS2_PLACEMENT_3D ( 'NONE', #18485, #7191, #2200 ) ;
#14277=CARTESIAN_POINT ( 'NONE',  ( -0.7600837003953544446, 18.55411937531343014, -136.0552959529982502 ) ) ;
#14285=ORIENTED_EDGE ( 'NONE', *, *, #5874, .F. ) ;
#14286=DIRECTION ( 'NONE',  ( 1.000000000000000000, -5.094701932209999624E-24, -2.257144641399999941E-12 ) ) ;
#14295=EDGE_LOOP ( 'NONE', ( #6724, #4650, #12924, #10440 ) ) ;
#14297=EDGE_CURVE ( 'NONE', #10668, #12077, #4991, .T. ) ;
#14308=CARTESIAN_POINT ( 'NONE',  ( 3.736991614122307848, -33.86279581096970759, -136.0552959530084536 ) ) ;
#14311=CARTESIAN_POINT ( 'NONE',  ( 6.750000000030000002, -33.75000000000000000, -137.0552959530000123 ) ) ;
#14316=CARTESIAN_POINT ( 'NONE',  ( -4.576286989381322279, 23.28076054106353965, -136.0552959529896668 ) ) ;
#14323=PLANE ( 'NONE',  #4199 ) ;
#14342=DIRECTION ( 'NONE',  ( -2.257198259660000092E-12, 0.000000000000000000, -1.000000000000000000 ) ) ;
#14350=AXIS2_PLACEMENT_3D ( 'NONE', #6050, #13300, #4272 ) ;
#14357=ORIENTED_EDGE ( 'NONE', *, *, #21172, .F. ) ;
#14369=DIRECTION ( 'NONE',  ( 5.094701932209999624E-24, 1.000000000000000000, -1.149947916579999802E-35 ) ) ;
#14384=CARTESIAN_POINT ( 'NONE',  ( -5.499999999959999997, 44.50000000000000000, -136.0552959530000123 ) ) ;
#14397=DIRECTION ( 'NONE',  ( 2.257144641399999941E-12, -8.049635416090000264E-35, 1.000000000000000000 ) ) ;
#14412=CARTESIAN_POINT ( 'NONE',  ( -14.80365045915063327, -44.50000000000000711, -136.0552959530004387 ) ) ;
#14418=CARTESIAN_POINT ( 'NONE',  ( 25.50000000000000000, 22.50000000000000000, -136.0552959530000123 ) ) ;
#14439=AXIS2_PLACEMENT_3D ( 'NONE', #6946, #21829, #8836 ) ;
#14441=EDGE_LOOP ( 'NONE', ( #15336, #13801, #7008, #22899 ) ) ;
#14450=DIRECTION ( 'NONE',  ( 1.000000000000000000, 0.000000000000000000, -2.257120985840000117E-12 ) ) ;
#14457=AXIS2_PLACEMENT_3D ( 'NONE', #10701, #7266, #3583 ) ;
#14459=AXIS2_PLACEMENT_3D ( 'NONE', #12558, #19835, #10523 ) ;
#14460=EDGE_CURVE ( 'NONE', #19147, #18032, #19974, .T. ) ;
#14464=ORIENTED_EDGE ( 'NONE', *, *, #6683, .F. ) ;
#14467=LINE ( 'NONE', #8856, #825 ) ;
#14479=DIRECTION ( 'NONE',  ( 2.257144641397284947E-12, 2.714590281723094849E-24, 1.000000000000000000 ) ) ;
#14486=VERTEX_POINT ( 'NONE', #14384 ) ;
#14487=EDGE_CURVE ( 'NONE', #824, #19147, #1908, .T. ) ;
#14496=VERTEX_POINT ( 'NONE', #4024 ) ;
#14512=ORIENTED_EDGE ( 'NONE', *, *, #21780, .T. ) ;
#14515=AXIS2_PLACEMENT_3D ( 'NONE', #21085, #14286, #3462 ) ;
#14522=LINE ( 'NONE', #22007, #18226 ) ;
#14535=FACE_OUTER_BOUND ( 'NONE', #17952, .T. ) ;
#14556=CARTESIAN_POINT ( 'NONE',  ( 6.446555752746835566, -30.75005219093839415, -136.0552959530145642 ) ) ;
#14564=EDGE_LOOP ( 'NONE', ( #7939, #21400, #11244, #19678 ) ) ;
#14571=CARTESIAN_POINT ( 'NONE',  ( 3.611688725869999975E-11, 47.50000000000000000, -136.0552959530000123 ) ) ;
#14573=DIRECTION ( 'NONE',  ( 2.255973186040000320E-12, 0.000000000000000000, 1.000000000000000000 ) ) ;
#14599=VERTEX_POINT ( 'NONE', #15427 ) ;
#14614=CARTESIAN_POINT ( 'NONE',  ( 3.611688725869999975E-11, -50.50000000000000000, -136.0552959530000123 ) ) ;
#14615=DIRECTION ( 'NONE',  ( 2.257749542879999954E-12, 0.000000000000000000, 1.000000000000000000 ) ) ;
#14641=FILL_AREA_STYLE_COLOUR ( '', #14116 ) ;
#14645=DIRECTION ( 'NONE',  ( 0.000000000000000000, 1.000000000000000000, 0.000000000000000000 ) ) ;
#14653=CARTESIAN_POINT ( 'NONE',  ( 4.698860268592982337, -1.999999999999998224, -136.0552959530106421 ) ) ;
#14660=VECTOR ( 'NONE', #5777, 1000.000000000000000 ) ;
#14693=EDGE_LOOP ( 'NONE', ( #12100, #20577, #14255, #3461 ) ) ;
#14698=CARTESIAN_POINT ( 'NONE',  ( 32.00000000000000000, -21.03620104879999886, -137.0552959530000123 ) ) ;
#14699=EDGE_LOOP ( 'NONE', ( #1777, #8643, #14003, #9577 ) ) ;
#14704=LINE ( 'NONE', #3891, #8557 ) ;
#14716=EDGE_LOOP ( 'NONE', ( #17348, #16779, #21053, #15692 ) ) ;
#14741=CARTESIAN_POINT ( 'NONE',  ( -12.50000000000000000, 25.50000000000000000, -137.0552959530000123 ) ) ;
#14761=EDGE_LOOP ( 'NONE', ( #10906, #5447, #6905, #19426 ) ) ;
#14765=ADVANCED_FACE ( 'NONE', ( #19543 ), #12032, .F. ) ;
#14779=CARTESIAN_POINT ( 'NONE',  ( 13.66060904168811696, 34.09818317340324256, -136.0552959530308783 ) ) ;
#14785=ADVANCED_FACE ( 'NONE', ( #12945 ), #14968, .F. ) ;
#14821=CARTESIAN_POINT ( 'NONE',  ( 8.446000075299080478, 27.76013181716325207, -136.0552959530190549 ) ) ;
#14830=LINE ( 'NONE', #22089, #14660 ) ;
#14833=ORIENTED_EDGE ( 'NONE', *, *, #8434, .T. ) ;
#14835=CARTESIAN_POINT ( 'NONE',  ( -7.499999999969999109, 45.50000000000000000, -137.0552959530000123 ) ) ;
#14839=VERTEX_POINT ( 'NONE', #5805 ) ;
#14841=EDGE_LOOP ( 'NONE', ( #4161, #9907, #3290, #19778 ) ) ;
#14851=DIRECTION ( 'NONE',  ( -0.7633862853691523176, 0.6459422414661291079, 1.722923451730345384E-12 ) ) ;
#14862=DIRECTION ( 'NONE',  ( -1.000000000000000000, 5.094701932209999624E-24, 2.257144641399999941E-12 ) ) ;
#14879=CARTESIAN_POINT ( 'NONE',  ( 25.31684607429999900, -45.26810052439999765, -137.0552959530000123 ) ) ;
#14881=CARTESIAN_POINT ( 'NONE',  ( -3.765209112771370492, 42.50000000000001421, -136.0552959529914858 ) ) ;
#14888=EDGE_LOOP ( 'NONE', ( #9505, #19371 ) ) ;
#14893=ORIENTED_EDGE ( 'NONE', *, *, #22784, .T. ) ;
#14900=CARTESIAN_POINT ( 'NONE',  ( 12.57628698947108958, 35.71923945894556596, -136.0552959530283772 ) ) ;
#14914=EDGE_CURVE ( 'NONE', #2935, #18341, #11854, .T. ) ;
#14922=CARTESIAN_POINT ( 'NONE',  ( -13.86630785130000021, -50.50000000000000000, -136.0552959530000123 ) ) ;
#14926=ORIENTED_EDGE ( 'NONE', *, *, #9924, .F. ) ;
#14930=CARTESIAN_POINT ( 'NONE',  ( 8.750000000030000891, -42.36803398869999882, -136.0552959530000123 ) ) ;
#14937=CARTESIAN_POINT ( 'NONE',  ( 31.50000000000000000, -2.273736754430000208E-12, -136.0552959530000123 ) ) ;
#14968=PLANE ( 'NONE',  #20121 ) ;
#14973=VECTOR ( 'NONE', #20726, 1000.000000000000000 ) ;
#14975=CARTESIAN_POINT ( 'NONE',  ( 19.13369214859999801, 50.50000000000000000, -136.5552959530000123 ) ) ;
#14993=ADVANCED_FACE ( 'NONE', ( #8047 ), #19600, .F. ) ;
#14999=VERTEX_POINT ( 'NONE', #6625 ) ;
#15019=DIRECTION ( 'NONE',  ( 5.094701932209999624E-24, 1.000000000000000000, -1.149947916579999802E-35 ) ) ;
#15020=VERTEX_POINT ( 'NONE', #5317 ) ;
#15024=DIRECTION ( 'NONE',  ( 2.257157423930000049E-12, 0.000000000000000000, 1.000000000000000000 ) ) ;
#15032=CARTESIAN_POINT ( 'NONE',  ( -25.86630785129999666, -2.273736754430000208E-12, -136.0552959530000123 ) ) ;
#15039=VECTOR ( 'NONE', #1656, 1000.000000000000000 ) ;
#15054=VECTOR ( 'NONE', #20276, 1000.000000000000000 ) ;
#15055=FACE_OUTER_BOUND ( 'NONE', #22366, .T. ) ;
#15066=DIRECTION ( 'NONE',  ( 2.257305453670000045E-12, 0.000000000000000000, 1.000000000000000000 ) ) ;
#15067=EDGE_CURVE ( 'NONE', #11916, #683, #5409, .T. ) ;
#15080=EDGE_LOOP ( 'NONE', ( #5648, #16285, #7887, #17944 ) ) ;
#15085=VECTOR ( 'NONE', #1500, 1000.000000000000000 ) ;
#15089=CIRCLE ( 'NONE', #3322, 1.499999999999999556 ) ;
#15092=DIRECTION ( 'NONE',  ( 2.257157423930000049E-12, 0.000000000000000000, 1.000000000000000000 ) ) ;
#15122=EDGE_CURVE ( 'NONE', #7449, #16762, #14704, .T. ) ;
#15140=EDGE_CURVE ( 'NONE', #7002, #10448, #9327, .T. ) ;
#15144=DIRECTION ( 'NONE',  ( 2.257157423930000049E-12, 0.000000000000000000, 1.000000000000000000 ) ) ;
#15152=CARTESIAN_POINT ( 'NONE',  ( 3.190250522981681769, -4.257526301755348186, -136.0552959530071746 ) ) ;
#15155=EDGE_CURVE ( 'NONE', #20206, #17461, #3651, .T. ) ;
#15157=VECTOR ( 'NONE', #22688, 1000.000000000000000 ) ;
#15167=CARTESIAN_POINT ( 'NONE',  ( -32.50000000000000000, 21.50000000000000000, -136.5552959530000123 ) ) ;
#15173=FACE_BOUND ( 'NONE', #14888, .T. ) ;
#15180=VECTOR ( 'NONE', #9214, 1000.000000000000000 ) ;
#15185=PLANE ( 'NONE',  #2597 ) ;
#15189=ORIENTED_EDGE ( 'NONE', *, *, #16227, .F. ) ;
#15193=VERTEX_POINT ( 'NONE', #20307 ) ;
#15194=EDGE_LOOP ( 'NONE', ( #22800, #15310, #18942, #6155 ) ) ;
#15196=EDGE_CURVE ( 'NONE', #21201, #5099, #3640, .T. ) ;
#15200=VECTOR ( 'NONE', #8447, 1000.000000000000000 ) ;
#15201=VECTOR ( 'NONE', #16837, 1000.000000000000000 ) ;
#15205=AXIS2_PLACEMENT_3D ( 'NONE', #21884, #18186, #23194 ) ;
#15208=EDGE_CURVE ( 'NONE', #3901, #11841, #14830, .T. ) ;
#15220=LINE ( 'NONE', #22588, #6307 ) ;
#15223=ORIENTED_EDGE ( 'NONE', *, *, #5720, .F. ) ;
#15233=DIRECTION ( 'NONE',  ( 0.7633862853691523176, 0.6459422414661291079, -1.722923451730345384E-12 ) ) ;
#15235=DIRECTION ( 'NONE',  ( -0.7071067811865471286, -0.7071067811865477948, 1.595945597898661113E-12 ) ) ;
#15239=VERTEX_POINT ( 'NONE', #18504 ) ;
#15248=LINE ( 'NONE', #20261, #9385 ) ;
#15260=CARTESIAN_POINT ( 'NONE',  ( -15.00000000000000000, -43.00000000000000000, -137.0552959530000123 ) ) ;
#15263=DIRECTION ( 'NONE',  ( 1.000000000000000000, -5.094701932209999624E-24, 0.000000000000000000 ) ) ;
#15270=VECTOR ( 'NONE', #16188, 1000.000000000000000 ) ;
#15273=VERTEX_POINT ( 'NONE', #20768 ) ;
#15277=DIRECTION ( 'NONE',  ( 2.257749542879999954E-12, 0.000000000000000000, 1.000000000000000000 ) ) ;
#15298=ADVANCED_FACE ( 'NONE', ( #6007 ), #13617, .T. ) ;
#15302=VERTEX_POINT ( 'NONE', #20537 ) ;
#15306=DIRECTION ( 'NONE',  ( 5.094701932209999624E-24, 1.000000000000000000, -1.149947916579999802E-35 ) ) ;
#15307=ORIENTED_EDGE ( 'NONE', *, *, #8554, .T. ) ;
#15308=EDGE_LOOP ( 'NONE', ( #5582, #9760, #782, #20407 ) ) ;
#15310=ORIENTED_EDGE ( 'NONE', *, *, #5415, .F. ) ;
#15311=CARTESIAN_POINT ( 'NONE',  ( -23.18315392570000100, 51.50000000000000000, -137.0552959530000123 ) ) ;
#15317=DIRECTION ( 'NONE',  ( 0.000000000000000000, 1.000000000000000000, 0.000000000000000000 ) ) ;
#15329=CARTESIAN_POINT ( 'NONE',  ( 1.133692148650000009, -50.50000000000000000, -136.0552959530000123 ) ) ;
#15330=ORIENTED_EDGE ( 'NONE', *, *, #1239, .F. ) ;
#15336=ORIENTED_EDGE ( 'NONE', *, *, #3766, .F. ) ;
#15349=ADVANCED_FACE ( 'NONE', ( #17191 ), #10033, .T. ) ;
#15350=ORIENTED_EDGE ( 'NONE', *, *, #14487, .T. ) ;
#15355=EDGE_LOOP ( 'NONE', ( #12703, #6364, #9446, #16734 ) ) ;
#15361=CARTESIAN_POINT ( 'NONE',  ( -16.49999999999998224, -42.80113973139842187, -136.0552959529627515 ) ) ;
#15363=LINE ( 'NONE', #12016, #7509 ) ;
#15373=ORIENTED_EDGE ( 'NONE', *, *, #19713, .F. ) ;
#15376=DIRECTION ( 'NONE',  ( 1.000000000000000000, 0.000000000000000000, -2.262079412673756451E-12 ) ) ;
#15381=ORIENTED_EDGE ( 'NONE', *, *, #8799, .T. ) ;
#15392=ADVANCED_FACE ( 'NONE', ( #2803 ), #22313, .F. ) ;
#15406=DIRECTION ( 'NONE',  ( -2.257144641399999941E-12, 0.000000000000000000, -1.000000000000000000 ) ) ;
#15409=ORIENTED_EDGE ( 'NONE', *, *, #9531, .F. ) ;
#15419=FACE_OUTER_BOUND ( 'NONE', #12678, .T. ) ;
#15424=CARTESIAN_POINT ( 'NONE',  ( -25.86630785129999666, -51.50000000000000000, -136.0552959530000123 ) ) ;
#15427=CARTESIAN_POINT ( 'NONE',  ( 6.500000000030000002, 28.00000000000000000, -137.0552959530000123 ) ) ;
#15436=DIRECTION ( 'NONE',  ( 1.000000000000000000, -5.094701932209999624E-24, -2.257144641399999941E-12 ) ) ;
#15438=CARTESIAN_POINT ( 'NONE',  ( -12.50000000000000000, 48.50000000000000000, -137.0552959530000123 ) ) ;
#15475=CARTESIAN_POINT ( 'NONE',  ( 4.750000000030000002, -44.75000000000000000, -136.0552959530000123 ) ) ;
#15476=ADVANCED_FACE ( 'NONE', ( #17907 ), #5059, .F. ) ;
#15480=LINE ( 'NONE', #22738, #738 ) ;
#15523=PLANE ( 'NONE',  #3795 ) ;
#15530=ORIENTED_EDGE ( 'NONE', *, *, #15670, .T. ) ;
#15539=CARTESIAN_POINT ( 'NONE',  ( 3.175121949296230373, 27.24084097722929343, -136.0552959530071746 ) ) ;
#15541=ORIENTED_EDGE ( 'NONE', *, *, #15155, .F. ) ;
#15565=DIRECTION ( 'NONE',  ( 2.257157423930000049E-12, 0.000000000000000000, 1.000000000000000000 ) ) ;
#15572=VECTOR ( 'NONE', #4363, 1000.000000000000000 ) ;
#15575=ORIENTED_EDGE ( 'NONE', *, *, #7618, .F. ) ;
#15578=B_SPLINE_CURVE_WITH_KNOTS ( 'NONE', 1,
 ( #6739, #11972 ),
 .UNSPECIFIED., .F., .F.,
 ( 2, 2 ),
 ( -8.099639781629999646, 8.099639781629999646 ),
 .UNSPECIFIED. ) ;
#15595=PLANE ( 'NONE',  #19362 ) ;
#15599=CARTESIAN_POINT ( 'NONE',  ( 32.50000000000000000, -21.03620104879999886, -136.5552959530000123 ) ) ;
#15613=CYLINDRICAL_SURFACE ( 'NONE', #500, 7.500000000000006217 ) ;
#15616=PRODUCT_DEFINITION_SHAPE ( 'NONE', 'NONE',  #1805 ) ;
#15621=ORIENTED_EDGE ( 'NONE', *, *, #12729, .F. ) ;
#15623=DIRECTION ( 'NONE',  ( -1.000000000000000000, 0.000000000000000000, 2.273736754430000208E-12 ) ) ;
#15624=CARTESIAN_POINT ( 'NONE',  ( -13.86630785130000021, -51.50000000000000000, -136.5552959530000123 ) ) ;
#15627=VECTOR ( 'NONE', #14007, 1000.000000000000000 ) ;
#15644=ORIENTED_EDGE ( 'NONE', *, *, #3505, .F. ) ;
#15656=DIRECTION ( 'NONE',  ( 2.257157423930000049E-12, 0.000000000000000000, 1.000000000000000000 ) ) ;
#15661=EDGE_CURVE ( 'NONE', #5099, #7733, #3973, .T. ) ;
#15662=AXIS2_PLACEMENT_3D ( 'NONE', #14930, #897, #20757 ) ;
#15670=EDGE_CURVE ( 'NONE', #20191, #2000, #9303, .T. ) ;
#15674=ADVANCED_FACE ( 'NONE', ( #20169 ), #5412, .F. ) ;
#15679=VERTEX_POINT ( 'NONE', #8958 ) ;
#15683=VERTEX_POINT ( 'NONE', #11206 ) ;
#15687=LINE ( 'NONE', #11979, #1079 ) ;
#15692=ORIENTED_EDGE ( 'NONE', *, *, #10611, .F. ) ;
#15695=VERTEX_POINT ( 'NONE', #1972 ) ;
#15704=CARTESIAN_POINT ( 'NONE',  ( -1.499999999959999553, 44.76558107705088929, -136.0552959529966301 ) ) ;
#15707=DIRECTION ( 'NONE',  ( 2.257144641397284947E-12, 2.714590281723094849E-24, 1.000000000000000000 ) ) ;
#15722=CARTESIAN_POINT ( 'NONE',  ( 25.50000000000000000, -2.273736754430000208E-12, -136.0552959530000123 ) ) ;
#15726=VERTEX_POINT ( 'NONE', #19814 ) ;
#15728=VECTOR ( 'NONE', #21058, 1000.000000000000000 ) ;
#15736=DIRECTION ( 'NONE',  ( 1.000000000000000000, -5.094701932209999624E-24, 0.000000000000000000 ) ) ;
#15752=ADVANCED_FACE ( 'NONE', ( #12657 ), #19925, .T. ) ;
#15756=DIRECTION ( 'NONE',  ( 1.000000000000000000, 0.000000000000000000, -2.262079412673756451E-12 ) ) ;
#15763=CARTESIAN_POINT ( 'NONE',  ( 5.523675324947334708, -46.35111558253264263, -136.0552959530124610 ) ) ;
#15768=EDGE_CURVE ( 'NONE', #19021, #15273, #13010, .T. ) ;
#15773=FILL_AREA_STYLE_COLOUR ( '', #19068 ) ;
#15775=VECTOR ( 'NONE', #4760, 1000.000000000000000 ) ;
#15787=EDGE_CURVE ( 'NONE', #6748, #7133, #20043, .T. ) ;
#15788=CARTESIAN_POINT ( 'NONE',  ( 4.892621826548920083, -4.960959015002474715, -136.0552959530008934 ) ) ;
#15792=EDGE_LOOP ( 'NONE', ( #20278, #23445, #15970, #4784 ) ) ;
#15794=EDGE_CURVE ( 'NONE', #2684, #22598, #4436, .T. ) ;
#15799=EDGE_CURVE ( 'NONE', #15020, #2120, #17043, .T. ) ;
#15801=LINE ( 'NONE', #8420, #19368 ) ;
#15813=CARTESIAN_POINT ( 'NONE',  ( 31.50000000000000000, 40.03620104880000241, -137.0552959530000123 ) ) ;
#15838=CIRCLE ( 'NONE', #19652, 7.499999999999999112 ) ;
#15857=ORIENTED_EDGE ( 'NONE', *, *, #19892, .F. ) ;
#15863=VERTEX_POINT ( 'NONE', #22290 ) ;
#15864=CARTESIAN_POINT ( 'NONE',  ( -12.50000000000000000, 19.50000000000000000, -136.0552959530000123 ) ) ;
#15876=FACE_OUTER_BOUND ( 'NONE', #4035, .T. ) ;
#15880=ORIENTED_EDGE ( 'NONE', *, *, #13206, .F. ) ;
#15904=DIRECTION ( 'NONE',  ( -1.000000000000000000, 0.000000000000000000, 2.257120985840000117E-12 ) ) ;
#15907=AXIS2_PLACEMENT_3D ( 'NONE', #851, #20249, #18563 ) ;
#15917=ADVANCED_FACE ( 'NONE', ( #4557 ), #639, .T. ) ;
#15918=CARTESIAN_POINT ( 'NONE',  ( -4.510096969185095617, 46.24633263602936495, -136.0552959529898374 ) ) ;
#15934=LINE ( 'NONE', #23198, #1091 ) ;
#15947=VECTOR ( 'NONE', #5565, 1000.000000000000000 ) ;
#15951=CIRCLE ( 'NONE', #14048, 1.499999999999999556 ) ;
#15952=PLANE ( 'NONE',  #8301 ) ;
#15953=VECTOR ( 'NONE', #16543, 1000.000000000000000 ) ;
#15954=ORIENTED_EDGE ( 'NONE', *, *, #14297, .F. ) ;
#15955=DIRECTION ( 'NONE',  ( 5.094701932209999624E-24, 1.000000000000000000, 0.000000000000000000 ) ) ;
#15959=DIRECTION ( 'NONE',  ( 2.257157423930000049E-12, 0.000000000000000000, 1.000000000000000000 ) ) ;
#15962=DIRECTION ( 'NONE',  ( 2.257144641397284947E-12, 2.714760815920564689E-24, 1.000000000000000000 ) ) ;
#15963=EDGE_CURVE ( 'NONE', #3707, #9912, #17751, .T. ) ;
#15964=CARTESIAN_POINT ( 'NONE',  ( 19.00000000000000000, 39.50000000000000000, -137.0552959530000123 ) ) ;
#15967=AXIS2_PLACEMENT_3D ( 'NONE', #6238, #18970, #15756 ) ;
#15970=ORIENTED_EDGE ( 'NONE', *, *, #199, .F. ) ;
#15972=LINE ( 'NONE', #6686, #12380 ) ;
#15979=CARTESIAN_POINT ( 'NONE',  ( 4.523700915383287224, -35.78365992287999120, -136.0552959530101589 ) ) ;
#15982=AXIS2_PLACEMENT_3D ( 'NONE', #12528, #3504, #8952 ) ;
#15983=CARTESIAN_POINT ( 'NONE',  ( 17.88103053862789693, 20.98519100496283940, -136.0552959530403996 ) ) ;
#15991=LINE ( 'NONE', #23252, #12149 ) ;
#16000=CARTESIAN_POINT ( 'NONE',  ( -3.499999999959999997, 44.50000000000000000, -136.0552959530000123 ) ) ;
#16006=CARTESIAN_POINT ( 'NONE',  ( -32.50000000000000000, 47.50000000000000000, -137.0552959530000123 ) ) ;
#16008=SURFACE_STYLE_USAGE ( .BOTH. , #8734 ) ;
#16017=ORIENTED_EDGE ( 'NONE', *, *, #15140, .F. ) ;
#16030=CARTESIAN_POINT ( 'NONE',  ( 6.500000000040000003, 20.50000000000000000, -136.0552959530000123 ) ) ;
#16039=VERTEX_POINT ( 'NONE', #12036 ) ;
#16051=AXIS2_PLACEMENT_3D ( 'NONE', #11622, #13789, #22832 ) ;
#16054=VECTOR ( 'NONE', #5796, 1000.000000000000000 ) ;
#16065=CARTESIAN_POINT ( 'NONE',  ( 3.175226512005099533, 13.75903940329188480, -136.0552959530071746 ) ) ;
#16074=ADVANCED_FACE ( 'NONE', ( #3353 ), #5133, .T. ) ;
#16079=EDGE_CURVE ( 'NONE', #2684, #10468, #15972, .T. ) ;
#16086=ORIENTED_EDGE ( 'NONE', *, *, #16824, .T. ) ;
#16087=EDGE_CURVE ( 'NONE', #8740, #15695, #13946, .T. ) ;
#16100=CARTESIAN_POINT ( 'NONE',  ( 9.763108217368069219, -33.86272049728325584, -136.0552959530220392 ) ) ;
#16103=EDGE_CURVE ( 'NONE', #23517, #6964, #13270, .T. ) ;
#16104=CARTESIAN_POINT ( 'NONE',  ( 18.66051412337919757, 24.90191174485666181, -136.0552959530421617 ) ) ;
#16106=EDGE_CURVE ( 'NONE', #4774, #15020, #20988, .T. ) ;
#16111=CARTESIAN_POINT ( 'NONE',  ( -5.660609041603422931, 24.90181682660472973, -136.0552959529872510 ) ) ;
#16116=DIRECTION ( 'NONE',  ( 2.255973186040000320E-12, 0.000000000000000000, 1.000000000000000000 ) ) ;
#16119=CARTESIAN_POINT ( 'NONE',  ( 8.750000000030000891, -44.75000000000000000, -136.0552959530000123 ) ) ;
#16125=DIRECTION ( 'NONE',  ( 1.000000000000000000, 0.000000000000000000, -2.257453483404485235E-12 ) ) ;
#16127=DIRECTION ( 'NONE',  ( 2.257749542879999954E-12, 0.000000000000000000, 1.000000000000000000 ) ) ;
#16131=VERTEX_POINT ( 'NONE', #9280 ) ;
#16137=CARTESIAN_POINT ( 'NONE',  ( 13.00952979664376130, 24.25756286941559026, -136.0552959530293720 ) ) ;
#16143=DIRECTION ( 'NONE',  ( -1.000000000000000000, 5.094701932209999624E-24, 2.257144641399999941E-12 ) ) ;
#16163=CARTESIAN_POINT ( 'NONE',  ( -5.101475126912967006, 45.72676979428531041, -136.0552959529885015 ) ) ;
#16166=EDGE_LOOP ( 'NONE', ( #3071, #4057, #10054, #16086 ) ) ;
#16170=DIRECTION ( 'NONE',  ( 2.257144641399999941E-12, -8.049635416090000264E-35, 1.000000000000000000 ) ) ;
#16182=CARTESIAN_POINT ( 'NONE',  ( 1.133692148650000009, -51.00000000000000000, -137.0552959530000123 ) ) ;
#16188=DIRECTION ( 'NONE',  ( 2.255973186040000320E-12, 0.000000000000000000, 1.000000000000000000 ) ) ;
#16189=FACE_OUTER_BOUND ( 'NONE', #7951, .T. ) ;
#16199=FACE_OUTER_BOUND ( 'NONE', #20254, .T. ) ;
#16209=CARTESIAN_POINT ( 'NONE',  ( -15.50000000000000000, 47.50000000000000000, -137.0552959530000123 ) ) ;
#16219=CARTESIAN_POINT ( 'NONE',  ( 20.50000000000000000, 25.50000000000000000, -136.0552959530000123 ) ) ;
#16227=EDGE_CURVE ( 'NONE', #16611, #21713, #612, .T. ) ;
#16242=VECTOR ( 'NONE', #18460, 1000.000000000000000 ) ;
#16245=DIRECTION ( 'NONE',  ( 1.000000000000000000, 0.000000000000000000, -2.257453483404485639E-12 ) ) ;
#16246=CARTESIAN_POINT ( 'NONE',  ( -12.50000000000000000, 22.50000000000000000, -137.0552959530000123 ) ) ;
#16285=ORIENTED_EDGE ( 'NONE', *, *, #10435, .T. ) ;
#16303=CARTESIAN_POINT ( 'NONE',  ( 5.519360106986514580, 13.04803137664692336, -136.0552959530124895 ) ) ;
#16311=CARTESIAN_POINT ( 'NONE',  ( -14.07987191918735270, -41.79896944934834124, -136.0552959529682084 ) ) ;
#16317=EDGE_CURVE ( 'NONE', #1507, #10304, #9391, .T. ) ;
#16324=DIRECTION ( 'NONE',  ( 1.000000000000000000, -5.094701932209999624E-24, -2.257144641399999941E-12 ) ) ;
#16325=EDGE_LOOP ( 'NONE', ( #8973, #5265, #18947, #11828 ) ) ;
#16332=VERTEX_POINT ( 'NONE', #2295 ) ;
#16342=CARTESIAN_POINT ( 'NONE',  ( 1.133692148650000009, 50.50000000000000000, -136.0552959530000123 ) ) ;
#16343=CARTESIAN_POINT ( 'NONE',  ( -4.576509874723263316, 21.71905350741257834, -136.0552959529896384 ) ) ;
#16344=AXIS2_PLACEMENT_3D ( 'NONE', #22196, #5883, #17186 ) ;
#16347=AXIS2_PLACEMENT_3D ( 'NONE', #9836, #7825, #9958 ) ;
#16363=CARTESIAN_POINT ( 'NONE',  ( 6.500000000040000003, 28.00000000000000000, -136.0552959530000123 ) ) ;
#16365=UNCERTAINTY_MEASURE_WITH_UNIT (LENGTH_MEASURE( 1.000000000000000082E-05 ), #10401, 'distance_accuracy_value', 'NONE');
#16385=DIRECTION ( 'NONE',  ( 2.257749542879999954E-12, 0.000000000000000000, 1.000000000000000000 ) ) ;
#16387=VERTEX_POINT ( 'NONE', #1437 ) ;
#16393=( GEOMETRIC_REPRESENTATION_CONTEXT ( 3 ) GLOBAL_UNCERTAINTY_ASSIGNED_CONTEXT ( ( #14226 ) ) GLOBAL_UNIT_ASSIGNED_CONTEXT ( ( #23332, #16648, #248 ) ) REPRESENTATION_CONTEXT ( 'NONE', 'WORKASPACE' ) );
#16399=EDGE_CURVE ( 'NONE', #20106, #19898, #965, .T. ) ;
#16408=DIRECTION ( 'NONE',  ( 1.000000000000000000, 0.000000000000000000, -2.253619677469999738E-12 ) ) ;
#16415=ORIENTED_EDGE ( 'NONE', *, *, #20551, .T. ) ;
#16421=CARTESIAN_POINT ( 'NONE',  ( -0.2408409771846180825, 17.17512194927200397, -136.0552959529995007 ) ) ;
#16426=EDGE_CURVE ( 'NONE', #19021, #17769, #13918, .T. ) ;
#16447=LINE ( 'NONE', #1949, #22790 ) ;
#16451=CARTESIAN_POINT ( 'NONE',  ( 9.660841442712255756, -32.96298433614438039, -136.0552959530218118 ) ) ;
#16457=LINE ( 'NONE', #9404, #11831 ) ;
#16463=CARTESIAN_POINT ( 'NONE',  ( 1.133692148650000009, 51.50000000000000000, -136.5552959530000123 ) ) ;
#16465=LINE ( 'NONE', #3856, #15054 ) ;
#16475=ADVANCED_FACE ( 'NONE', ( #2863 ), #19520, .F. ) ;
#16481=CARTESIAN_POINT ( 'NONE',  ( 7.750000000030000002, -37.98606797749999942, -136.0552959530000123 ) ) ;
#16482=ORIENTED_EDGE ( 'NONE', *, *, #2853, .F. ) ;
#16483=CARTESIAN_POINT ( 'NONE',  ( 25.50006728700737924, 36.10251055750465099, -136.0552959530575663 ) ) ;
#16484=EDGE_CURVE ( 'NONE', #12948, #5167, #13810, .T. ) ;
#16488=LINE ( 'NONE', #21746, #11414 ) ;
#16491=DIRECTION ( 'NONE',  ( 2.257157423930000049E-12, 0.000000000000000000, 1.000000000000000000 ) ) ;
#16496=ORIENTED_EDGE ( 'NONE', *, *, #22317, .T. ) ;
#16497=LINE ( 'NONE', #7448, #23488 ) ;
#16498=ORIENTED_EDGE ( 'NONE', *, *, #20586, .F. ) ;
#16511=CARTESIAN_POINT ( 'NONE',  ( 25.31684607429999900, 45.26810052439999765, -137.0552959530000123 ) ) ;
#16525=EDGE_CURVE ( 'NONE', #11605, #11936, #16526, .T. ) ;
#16526=LINE ( 'NONE', #234, #13102 ) ;
#16541=VECTOR ( 'NONE', #7369, 1000.000000000000000 ) ;
#16543=DIRECTION ( 'NONE',  ( -1.000000000000000000, 0.000000000000000000, 2.257120985840000117E-12 ) ) ;
#16547=ORIENTED_EDGE ( 'NONE', *, *, #1995, .F. ) ;
#16549=VERTEX_POINT ( 'NONE', #3683 ) ;
#16550=CARTESIAN_POINT ( 'NONE',  ( 6.000000000010004442, -3.300767767050150070, -136.0552959530135411 ) ) ;
#16560=CARTESIAN_POINT ( 'NONE',  ( 13.09808825521931297, 34.66051412330310200, -136.0552959530295993 ) ) ;
#16563=CYLINDRICAL_SURFACE ( 'NONE', #1243, 3.000000000000002665 ) ;
#16564=DIRECTION ( 'NONE',  ( 0.000000000000000000, 1.000000000000000000, 0.000000000000000000 ) ) ;
#16579=CARTESIAN_POINT ( 'NONE',  ( 3.611688725869999975E-11, 51.50000000000000000, -136.0552959530000123 ) ) ;
#16580=CARTESIAN_POINT ( 'NONE',  ( -25.86630785129999666, -50.50000000000000000, -137.0552959530000123 ) ) ;
#16592=CARTESIAN_POINT ( 'NONE',  ( 24.33948587669652497, 34.09808825513344743, -136.0552959530549515 ) ) ;
#16593=LINE ( 'NONE', #7779, #398 ) ;
#16594=CYLINDRICAL_SURFACE ( 'NONE', #10553, 1.500000000000003331 ) ;
#16595=ORIENTED_EDGE ( 'NONE', *, *, #620, .F. ) ;
#16598=EDGE_CURVE ( 'NONE', #15273, #7002, #10796, .T. ) ;
#16606=VERTEX_POINT ( 'NONE', #23318 ) ;
#16609=EDGE_LOOP ( 'NONE', ( #1630, #1866 ) ) ;
#16611=VERTEX_POINT ( 'NONE', #7010 ) ;
#16629=VECTOR ( 'NONE', #415, 1000.000000000000000 ) ;
#16635=EDGE_CURVE ( 'NONE', #20206, #7723, #11575, .T. ) ;
#16644=CARTESIAN_POINT ( 'NONE',  ( 6.000000000010000001, -3.500000000000000000, -137.0552959530000123 ) ) ;
#16648=( NAMED_UNIT ( * ) PLANE_ANGLE_UNIT ( ) SI_UNIT ( $, .RADIAN. ) );
#16665=CIRCLE ( 'NONE', #6402, 1.499999999999999556 ) ;
#16671=DIRECTION ( 'NONE',  ( 2.256861364460000137E-12, 0.000000000000000000, 1.000000000000000000 ) ) ;
#16673=VECTOR ( 'NONE', #5205, 1000.000000000000000 ) ;
#16678=EDGE_CURVE ( 'NONE', #7477, #16880, #12888, .T. ) ;
#16688=ORIENTED_EDGE ( 'NONE', *, *, #2257, .T. ) ;
#16693=VERTEX_POINT ( 'NONE', #18027 ) ;
#16700=AXIS2_PLACEMENT_3D ( 'NONE', #4649, #11891, #11530 ) ;
#16701=ORIENTED_EDGE ( 'NONE', *, *, #20108, .T. ) ;
#16710=DIRECTION ( 'NONE',  ( 0.000000000000000000, -1.000000000000000000, 0.000000000000000000 ) ) ;
#16718=B_SPLINE_CURVE_WITH_KNOTS ( 'NONE', 3,
 ( #17866, #14412, #7146, #19890, #5486, #142, #12618, #3823, #7384, #1935 ),
 .UNSPECIFIED., .F., .F.,
 ( 4, 2, 2, 2, 4 ),
 ( 0.000000000000000000, 0.2500000000000000000, 0.5000000000000000000, 0.7500000000000000000, 1.000000000000000000 ),
 .UNSPECIFIED. ) ;
#16725=VERTEX_POINT ( 'NONE', #12537 ) ;
#16734=ORIENTED_EDGE ( 'NONE', *, *, #19490, .T. ) ;
#16736=EDGE_CURVE ( 'NONE', #15302, #7477, #1738, .T. ) ;
#16751=DIRECTION ( 'NONE',  ( 2.257157423930000049E-12, 0.000000000000000000, 1.000000000000000000 ) ) ;
#16757=DIRECTION ( 'NONE',  ( -1.000000000000000000, 5.094701932209999624E-24, 2.257144641399999941E-12 ) ) ;
#16759=EDGE_LOOP ( 'NONE', ( #17466, #8282, #3642, #3146 ) ) ;
#16762=VERTEX_POINT ( 'NONE', #12189 ) ;
#16779=ORIENTED_EDGE ( 'NONE', *, *, #20615, .T. ) ;
#16790=LINE ( 'NONE', #18235, #11654 ) ;
#16799=CARTESIAN_POINT ( 'NONE',  ( 15.10234832544105643, 33.50000000000002132, -136.0552959530340331 ) ) ;
#16809=EDGE_CURVE ( 'NONE', #8740, #416, #3629, .T. ) ;
#16811=EDGE_CURVE ( 'NONE', #8391, #19898, #9073, .T. ) ;
#16815=ORIENTED_EDGE ( 'NONE', *, *, #13877, .T. ) ;
#16824=EDGE_CURVE ( 'NONE', #15695, #8634, #20396, .T. ) ;
#16837=DIRECTION ( 'NONE',  ( 2.259525899719999991E-12, 0.000000000000000000, 1.000000000000000000 ) ) ;
#16840=CARTESIAN_POINT ( 'NONE',  ( 13.05339791269693528, 16.72285764721824819, -136.0552959530147348 ) ) ;
#16844=CARTESIAN_POINT ( 'NONE',  ( 32.50000000000000000, -40.50000000000000000, -137.0552959530000123 ) ) ;
#16845=ADVANCED_FACE ( 'NONE', ( #20048 ), #21727, .T. ) ;
#16849=ORIENTED_EDGE ( 'NONE', *, *, #19791, .T. ) ;
#16853=ORIENTED_EDGE ( 'NONE', *, *, #9220, .F. ) ;
#16856=PLANE ( 'NONE',  #20860 ) ;
#16872=ORIENTED_EDGE ( 'NONE', *, *, #16525, .F. ) ;
#16880=VERTEX_POINT ( 'NONE', #178 ) ;
#16895=CARTESIAN_POINT ( 'NONE',  ( 19.13369214859999801, 50.50000000000000000, -137.0552959530000123 ) ) ;
#16897=ADVANCED_BREP_SHAPE_REPRESENTATION ( '', ( #12179, #5025 ), #1616 ) ;
#16918=EDGE_LOOP ( 'NONE', ( #9366, #3433, #21570, #5449 ) ) ;
#16921=ORIENTED_EDGE ( 'NONE', *, *, #19443, .T. ) ;
#16934=LINE ( 'NONE', #15032, #8650 ) ;
#16943=AXIS2_PLACEMENT_3D ( 'NONE', #20742, #4210, #9656 ) ;
#16948=DIRECTION ( 'NONE',  ( 1.000000000000000000, -5.094701932209999624E-24, 0.000000000000000000 ) ) ;
#16963=ORIENTED_EDGE ( 'NONE', *, *, #8488, .F. ) ;
#16970=ORIENTED_EDGE ( 'NONE', *, *, #16736, .F. ) ;
#16974=AXIS2_PLACEMENT_3D ( 'NONE', #2255, #14862, #6363 ) ;
#16976=DIRECTION ( 'NONE',  ( 1.000000000000000000, 0.000000000000000000, -2.257157423930000049E-12 ) ) ;
#16987=FACE_OUTER_BOUND ( 'NONE', #3647, .T. ) ;
#16991=CARTESIAN_POINT ( 'NONE',  ( 3.611688725869999975E-11, -51.50000000000000000, -136.0552959530000123 ) ) ;
#17003=DIRECTION ( 'NONE',  ( 1.000000000000000000, 0.000000000000000000, -2.257453483404485235E-12 ) ) ;
#17018=CARTESIAN_POINT ( 'NONE',  ( 4.500000000009999113, -3.500000000000000000, -137.0552959530000123 ) ) ;
#17032=VERTEX_POINT ( 'NONE', #13595 ) ;
#17034=LINE ( 'NONE', #13350, #21394 ) ;
#17043=LINE ( 'NONE', #4326, #7814 ) ;
#17046=CARTESIAN_POINT ( 'NONE',  ( -13.50000000000000000, -43.00000000000000000, -136.5552959530000123 ) ) ;
#17068=LINE ( 'NONE', #22554, #4931 ) ;
#17084=DIRECTION ( 'NONE',  ( 0.000000000000000000, 0.000000000000000000, 1.000000000000000000 ) ) ;
#17089=CARTESIAN_POINT ( 'NONE',  ( -0.009371101328294257835, 24.25767361204308870, -136.0552959530000123 ) ) ;
#17114=VECTOR ( 'NONE', #8516, 1000.000000000000000 ) ;
#17117=CYLINDRICAL_SURFACE ( 'NONE', #16051, 2.999999999999999112 ) ;
#17124=ORIENTED_EDGE ( 'NONE', *, *, #16106, .F. ) ;
#17131=CARTESIAN_POINT ( 'NONE',  ( -16.50000000000000000, -43.00000000000000000, -136.0552959530000123 ) ) ;
#17147=CLOSED_SHELL ( 'NONE', ( #11212, #11696, #20477, #21439, #20733, #6015, #16074, #11534, #16475, #1558, #21782, #18626, #12156, #13792, #11480, #1923, #14765, #15392, #2723, #15674, #4312, #3412, #14993, #7726, #10621, #4136, #1339, #12515, #22064, #9793, #12427, #12005, #15476, #3420, #11248, #18834, #22004, #9388, #21043, #12027, #2286, #7744, #7487, #14043, #23277, #9899, #21464, #2141, #1362, #20374, #14785, #4289, #9227, #13590, #6074, #16845, #15917, #15298, #19051, #15752, #5776, #23471, #10373, #1703, #1033, #20452, #2430, #1937, #5873, #15349, #14020, #7363, #10387, #6333, #6335, #21756, #9034, #8599, #11747, #13846 ) ) ;
#17157=FACE_OUTER_BOUND ( 'NONE', #376, .T. ) ;
#17162=VECTOR ( 'NONE', #3847, 1000.000000000000000 ) ;
#17183=B_SPLINE_CURVE_WITH_KNOTS ( 'NONE', 3,
 ( #11715, #19223, #20781, #10292, #10044, #1036, #17089, #1165, #13986, #2932, #4596, #21144, #15539, #17441, #1282, #8266, #2704, #11839 ),
 .UNSPECIFIED., .F., .F.,
 ( 4, 2, 2, 2, 2, 2, 2, 2, 4 ),
 ( 0.000000000000000000, 0.1250000000000000278, 0.2500000000000000555, 0.3750000000000001110, 0.5000000000000001110, 0.6250000000000001110, 0.7500000000000002220, 0.8750000000000001110, 1.000000000000000000 ),
 .UNSPECIFIED. ) ;
#17186=DIRECTION ( 'NONE',  ( -1.000000000000000000, 5.094701932209999624E-24, 0.000000000000000000 ) ) ;
#17191=FACE_OUTER_BOUND ( 'NONE', #4000, .T. ) ;
#17204=DIRECTION ( 'NONE',  ( 2.255973186040000320E-12, 0.000000000000000000, 1.000000000000000000 ) ) ;
#17208=LINE ( 'NONE', #4252, #15572 ) ;
#17216=DIRECTION ( 'NONE',  ( 2.257144641399999941E-12, -8.049635416090000264E-35, 1.000000000000000000 ) ) ;
#17217=EDGE_CURVE ( 'NONE', #17032, #16762, #19046, .T. ) ;
#17219=CARTESIAN_POINT ( 'NONE',  ( -13.86630785130000021, -51.00000000000000000, -136.0552959530000123 ) ) ;
#17228=CARTESIAN_POINT ( 'NONE',  ( -12.50000000000000000, 19.50000000000000000, -137.0552959530000123 ) ) ;
#17231=AXIS2_PLACEMENT_3D ( 'NONE', #20185, #7543, #10999 ) ;
#17256=CARTESIAN_POINT ( 'NONE',  ( -16.50000000000000000, -43.00000000000000000, -137.0552959530000123 ) ) ;
#17273=LINE ( 'NONE', #19418, #20317 ) ;
#17276=CARTESIAN_POINT ( 'NONE',  ( 23.50000000000000000, -20.50000000000000000, -137.2152959530000089 ) ) ;
#17309=DIRECTION ( 'NONE',  ( 2.257144641397284947E-12, 2.714724913984255017E-24, 1.000000000000000000 ) ) ;
#17315=VECTOR ( 'NONE', #22204, 1000.000000000000000 ) ;
#17325=CARTESIAN_POINT ( 'NONE',  ( 19.13369214859999801, -50.50000000000000000, -136.0552959530000123 ) ) ;
#17332=CARTESIAN_POINT ( 'NONE',  ( -13.86630785130000021, -50.50000000000000000, -137.0552959530000123 ) ) ;
#17348=ORIENTED_EDGE ( 'NONE', *, *, #4274, .F. ) ;
#17354=ORIENTED_EDGE ( 'NONE', *, *, #11164, .T. ) ;
#17356=LINE ( 'NONE', #19742, #5421 ) ;
#17363=VERTEX_POINT ( 'NONE', #2987 ) ;
#17364=VECTOR ( 'NONE', #12891, 1000.000000000000000 ) ;
#17369=DIRECTION ( 'NONE',  ( 1.000000000000000000, -5.094701932209999624E-24, 0.000000000000000000 ) ) ;
#17376=DIRECTION ( 'NONE',  ( 5.094701932209999624E-24, 1.000000000000000000, -1.149947916579999802E-35 ) ) ;
#17381=ORIENTED_EDGE ( 'NONE', *, *, #9226, .T. ) ;
#17382=PLANE ( 'NONE',  #14515 ) ;
#17383=EDGE_CURVE ( 'NONE', #11841, #8740, #21312, .T. ) ;
#17394=ORIENTED_EDGE ( 'NONE', *, *, #3416, .F. ) ;
#17408=ORIENTED_EDGE ( 'NONE', *, *, #16426, .T. ) ;
#17432=ORIENTED_EDGE ( 'NONE', *, *, #21896, .F. ) ;
#17441=CARTESIAN_POINT ( 'NONE',  ( 4.084326842555937809, 27.61765588495817525, -136.0552959530091641 ) ) ;
#17461=VERTEX_POINT ( 'NONE', #21196 ) ;
#17466=ORIENTED_EDGE ( 'NONE', *, *, #20586, .T. ) ;
#17475=DIRECTION ( 'NONE',  ( 0.000000000000000000, -1.000000000000000000, 0.000000000000000000 ) ) ;
#17477=VECTOR ( 'NONE', #9490, 1000.000000000000000 ) ;
#17486=ORIENTED_EDGE ( 'NONE', *, *, #17951, .T. ) ;
#17487=VECTOR ( 'NONE', #21555, 1000.000000000000000 ) ;
#17511=LINE ( 'NONE', #1234, #2025 ) ;
#17514=PLANE ( 'NONE',  #10661 ) ;
#17517=CARTESIAN_POINT ( 'NONE',  ( 15.50000000000000000, 39.50000000000000000, -136.5552959530000123 ) ) ;
#17524=CARTESIAN_POINT ( 'NONE',  ( 19.00000000000000000, 33.50000000000000000, -136.0552959530000123 ) ) ;
#17553=CARTESIAN_POINT ( 'NONE',  ( 7.759759976971661644, -46.49600213680211169, -136.0552959530175201 ) ) ;
#17562=DIRECTION ( 'NONE',  ( 5.094701932209999624E-24, 1.000000000000000000, -1.149947916579999802E-35 ) ) ;
#17580=ORIENTED_EDGE ( 'NONE', *, *, #2686, .T. ) ;
#17585=CARTESIAN_POINT ( 'NONE',  ( 5.421820079972371254, -4.699500263597272465, -136.0552959530021155 ) ) ;
#17594=PLANE ( 'NONE',  #2759 ) ;
#17603=LINE ( 'NONE', #22600, #19862 ) ;
#17611=ORIENTED_EDGE ( 'NONE', *, *, #4274, .T. ) ;
#17642=CARTESIAN_POINT ( 'NONE',  ( -15.50000000000000000, 34.50000000000000000, -137.0552959530000123 ) ) ;
#17653=ORIENTED_EDGE ( 'NONE', *, *, #1906, .F. ) ;
#17665=CARTESIAN_POINT ( 'NONE',  ( 4.800813058695553970, -45.27045733082635337, -136.0552959530108410 ) ) ;
#17668=CARTESIAN_POINT ( 'NONE',  ( 4.750000000030000002, -44.75000000000000000, -137.0552959530000123 ) ) ;
#17677=AXIS2_PLACEMENT_3D ( 'NONE', #1504, #12307, #16125 ) ;
#17684=EDGE_CURVE ( 'NONE', #1522, #20239, #15220, .T. ) ;
#17702=ORIENTED_EDGE ( 'NONE', *, *, #22446, .F. ) ;
#17708=CARTESIAN_POINT ( 'NONE',  ( -3.499999999959999997, 46.50000000000000000, -136.0552959530000123 ) ) ;
#17713=VECTOR ( 'NONE', #587, 1000.000000000000000 ) ;
#17721=VERTEX_POINT ( 'NONE', #4037 ) ;
#17729=LINE ( 'NONE', #15599, #15200 ) ;
#17733=DIRECTION ( 'NONE',  ( 2.257749542879999954E-12, 0.000000000000000000, 1.000000000000000000 ) ) ;
#17734=ORIENTED_EDGE ( 'NONE', *, *, #16598, .T. ) ;
#17736=CARTESIAN_POINT ( 'NONE',  ( -14.60932014329231343, -41.53824377979346139, -136.0552959529670716 ) ) ;
#17749=ORIENTED_EDGE ( 'NONE', *, *, #10598, .F. ) ;
#17751=LINE ( 'NONE', #21453, #13522 ) ;
#17759=ORIENTED_EDGE ( 'NONE', *, *, #11857, .T. ) ;
#17764=VECTOR ( 'NONE', #21267, 1000.000000000000000 ) ;
#17769=VERTEX_POINT ( 'NONE', #11389 ) ;
#17773=LINE ( 'NONE', #23257, #21707 ) ;
#17778=CARTESIAN_POINT ( 'NONE',  ( 8.698929461760148030, -45.27072668386799137, -136.0552959530196233 ) ) ;
#17779=EDGE_CURVE ( 'NONE', #16387, #3836, #9714, .T. ) ;
#17783=DIRECTION ( 'NONE',  ( 2.257157423930000049E-12, 0.000000000000000000, 1.000000000000000000 ) ) ;
#17784=CARTESIAN_POINT ( 'NONE',  ( -3.499999999959999997, 42.50000000000000000, -136.0552959530000123 ) ) ;
#17795=CARTESIAN_POINT ( 'NONE',  ( 25.00000000000000000, -20.50000000000000000, -137.2152959530000089 ) ) ;
#17797=DIRECTION ( 'NONE',  ( -2.257144641399999941E-12, 8.049635416090000264E-35, -1.000000000000000000 ) ) ;
#17801=LINE ( 'NONE', #21624, #17764 ) ;
#17808=VECTOR ( 'NONE', #16976, 1000.000000000000000 ) ;
#17811=AXIS2_PLACEMENT_3D ( 'NONE', #23032, #17562, #12752 ) ;
#17818=CARTESIAN_POINT ( 'NONE',  ( 8.750000000030000891, -2.273736754430000208E-12, -136.0552959530000123 ) ) ;
#17822=ORIENTED_EDGE ( 'NONE', *, *, #10074, .T. ) ;
#17829=VERTEX_POINT ( 'NONE', #4496 ) ;
#17862=CARTESIAN_POINT ( 'NONE',  ( -15.00000000000000000, -41.50000000000000000, -136.0552959530000123 ) ) ;
#17866=CARTESIAN_POINT ( 'NONE',  ( -15.00000000000000000, -44.50000000000000000, -136.0552959530000123 ) ) ;
#17883=CARTESIAN_POINT ( 'NONE',  ( 8.750000000030000891, -36.98606797749999942, -137.0552959530000123 ) ) ;
#17889=CARTESIAN_POINT ( 'NONE',  ( 19.71905350744767205, 19.57650987476679916, -136.0552959530445492 ) ) ;
#17898=CYLINDRICAL_SURFACE ( 'NONE', #15982, 1.500000000000001998 ) ;
#17904=VECTOR ( 'NONE', #2008, 1000.000000000000000 ) ;
#17905=CARTESIAN_POINT ( 'NONE',  ( 5.740346993259798580, -46.49619218629824502, -136.0552959530129726 ) ) ;
#17906=VECTOR ( 'NONE', #9296, 1000.000000000000000 ) ;
#17907=FACE_OUTER_BOUND ( 'NONE', #20539, .T. ) ;
#17917=DIRECTION ( 'NONE',  ( 5.094701932209999624E-24, 1.000000000000000000, 0.000000000000000000 ) ) ;
#17921=CARTESIAN_POINT ( 'NONE',  ( 3.611688725869999975E-11, 39.50000000000000000, -136.0552959530000123 ) ) ;
#17927=CARTESIAN_POINT ( 'NONE',  ( -7.499999999969999109, 19.50000000000000000, -136.5552959530000123 ) ) ;
#17929=FACE_OUTER_BOUND ( 'NONE', #14063, .T. ) ;
#17944=ORIENTED_EDGE ( 'NONE', *, *, #18279, .F. ) ;
#17951=EDGE_CURVE ( 'NONE', #7723, #14599, #7442, .T. ) ;
#17952=EDGE_LOOP ( 'NONE', ( #3525, #10320, #3398, #7147 ) ) ;
#17964=VERTEX_POINT ( 'NONE', #8636 ) ;
#17965=DIRECTION ( 'NONE',  ( 0.000000000000000000, 1.000000000000000000, 0.000000000000000000 ) ) ;
#17979=ORIENTED_EDGE ( 'NONE', *, *, #18385, .F. ) ;
#17982=DIRECTION ( 'NONE',  ( 2.257157423930000049E-12, 0.000000000000000000, 1.000000000000000000 ) ) ;
#17986=LINE ( 'NONE', #8916, #15953 ) ;
#18004=CARTESIAN_POINT ( 'NONE',  ( 8.201139657866018950, -31.10711941572444061, -136.0552959530184864 ) ) ;
#18017=VERTEX_POINT ( 'NONE', #12572 ) ;
#18018=DIRECTION ( 'NONE',  ( 1.000000000000000000, -5.094701932209999624E-24, 0.000000000000000000 ) ) ;
#18019=DIRECTION ( 'NONE',  ( -1.000000000000000000, 0.000000000000000000, 2.257120985840000117E-12 ) ) ;
#18020=CARTESIAN_POINT ( 'NONE',  ( 13.13369214870000157, -51.50000000000000000, -137.0552959530000123 ) ) ;
#18023=CIRCLE ( 'NONE', #11926, 1.499999999999999556 ) ;
#18024=DIRECTION ( 'NONE',  ( -1.000000000000000000, 0.000000000000000000, 2.257120985840000117E-12 ) ) ;
#18026=DIRECTION ( 'NONE',  ( -2.257144641399999941E-12, 8.049635416090000264E-35, -1.000000000000000000 ) ) ;
#18027=CARTESIAN_POINT ( 'NONE',  ( 20.50000000000000000, 19.50000000000000000, -137.0552959530000123 ) ) ;
#18028=PLANE ( 'NONE',  #7494 ) ;
#18030=ORIENTED_EDGE ( 'NONE', *, *, #6716, .F. ) ;
#18032=VERTEX_POINT ( 'NONE', #12449 ) ;
#18038=CARTESIAN_POINT ( 'NONE',  ( 13.24084097724100317, 23.82487805073530041, -136.0552959530298835 ) ) ;
#18046=FACE_BOUND ( 'NONE', #13465, .T. ) ;
#18061=EDGE_CURVE ( 'NONE', #18787, #14486, #20078, .T. ) ;
#18065=ORIENTED_EDGE ( 'NONE', *, *, #8488, .T. ) ;
#18074=ORIENTED_EDGE ( 'NONE', *, *, #21916, .F. ) ;
#18087=DIRECTION ( 'NONE',  ( 1.000000000000000000, 0.000000000000000000, -2.257453483404482811E-12 ) ) ;
#18094=ORIENTED_EDGE ( 'NONE', *, *, #199, .T. ) ;
#18096=DIRECTION ( 'NONE',  ( 2.257305453670000045E-12, 0.000000000000000000, 1.000000000000000000 ) ) ;
#18100=ORIENTED_EDGE ( 'NONE', *, *, #7618, .T. ) ;
#18101=FACE_OUTER_BOUND ( 'NONE', #18149, .T. ) ;
#18106=CARTESIAN_POINT ( 'NONE',  ( 3.298969449361869088, -2.579871919192233687, -136.0552959530074872 ) ) ;
#18119=CARTESIAN_POINT ( 'NONE',  ( 5.569521322453342194, -30.97557888555125771, -136.0552959530125463 ) ) ;
#18122=CARTESIAN_POINT ( 'NONE',  ( 20.50000000000000000, 19.50000000000000000, -136.0552959530000123 ) ) ;
#18124=AXIS2_PLACEMENT_3D ( 'NONE', #3628, #18026, #16245 ) ;
#18136=CARTESIAN_POINT ( 'NONE',  ( 32.50000000000000000, -27.03620104879999886, -137.0552959530000123 ) ) ;
#18137=VECTOR ( 'NONE', #18024, 1000.000000000000000 ) ;
#18138=EDGE_CURVE ( 'NONE', #17964, #2277, #19206, .T. ) ;
#18142=CARTESIAN_POINT ( 'NONE',  ( -4.499999999969999109, 34.00000000000000000, -136.5552959530000123 ) ) ;
#18145=DIRECTION ( 'NONE',  ( 2.257083409060000051E-12, 0.000000000000000000, 1.000000000000000000 ) ) ;
#18149=EDGE_LOOP ( 'NONE', ( #15307, #5357, #7392, #5552 ) ) ;
#18153=CARTESIAN_POINT ( 'NONE',  ( 12.15117705468384202, 25.45516771069291195, -136.0552959530274677 ) ) ;
#18162=FACE_BOUND ( 'NONE', #3198, .T. ) ;
#18186=DIRECTION ( 'NONE',  ( 2.257144641399999941E-12, -8.049635416090000264E-35, 1.000000000000000000 ) ) ;
#18191=ORIENTED_EDGE ( 'NONE', *, *, #15208, .F. ) ;
#18192=VECTOR ( 'NONE', #1332, 1000.000000000000000 ) ;
#18200=CARTESIAN_POINT ( 'NONE',  ( -24.00000000000000000, 47.50000000000000000, -137.0552959530000123 ) ) ;
#18204=CARTESIAN_POINT ( 'NONE',  ( 2.742326387988431424, 13.99062889862883097, -136.0552959530062083 ) ) ;
#18206=VECTOR ( 'NONE', #6383, 1000.000000000000000 ) ;
#18215=CYLINDRICAL_SURFACE ( 'NONE', #1173, 1.500000000000001110 ) ;
#18226=VECTOR ( 'NONE', #9482, 1000.000000000000000 ) ;
#18228=CARTESIAN_POINT ( 'NONE',  ( 4.300767767059650026, -1.999999999999999556, -136.0552959530097041 ) ) ;
#18234=AXIS2_PLACEMENT_3D ( 'NONE', #20246, #2160, #15235 ) ;
#18235=CARTESIAN_POINT ( 'NONE',  ( 13.13369214870000157, -51.00000000000000000, -137.0552959530000123 ) ) ;
#18242=CARTESIAN_POINT ( 'NONE',  ( 4.055709778280034428, -32.39604587945242997, -136.0552959530091641 ) ) ;
#18245=CARTESIAN_POINT ( 'NONE',  ( 4.500000000009999113, -5.000000000000000000, -136.0552959530000123 ) ) ;
#18248=CARTESIAN_POINT ( 'NONE',  ( -5.985028652370273150, 19.88109793996622443, -136.0552959529864552 ) ) ;
#18273=VERTEX_POINT ( 'NONE', #1622 ) ;
#18279=EDGE_CURVE ( 'NONE', #12078, #5331, #16465, .T. ) ;
#18281=FACE_OUTER_BOUND ( 'NONE', #9552, .T. ) ;
#18284=LINE ( 'NONE', #192, #6778 ) ;
#18293=VERTEX_POINT ( 'NONE', #5518 ) ;
#18294=LINE ( 'NONE', #3656, #17904 ) ;
#18314=LINE ( 'NONE', #19751, #12875 ) ;
#18325=LINE ( 'NONE', #2037, #20822 ) ;
#18341=VERTEX_POINT ( 'NONE', #18020 ) ;
#18342=DIRECTION ( 'NONE',  ( 0.000000000000000000, 8.018988631039999700E-27, -1.000000000000000000 ) ) ;
#18365=ORIENTED_EDGE ( 'NONE', *, *, #3234, .T. ) ;
#18368=CARTESIAN_POINT ( 'NONE',  ( -12.50000000000000000, 42.50000000000000000, -136.5552959530000123 ) ) ;
#18376=DIRECTION ( 'NONE',  ( 0.000000000000000000, 1.000000000000000000, 0.000000000000000000 ) ) ;
#18378=CARTESIAN_POINT ( 'NONE',  ( 4.500000000009999113, -5.000000000000000000, -136.0552959530000123 ) ) ;
#18383=DIRECTION ( 'NONE',  ( 2.257749542879999954E-12, 0.000000000000000000, 1.000000000000000000 ) ) ;
#18385=EDGE_CURVE ( 'NONE', #16693, #4825, #23489, .T. ) ;
#18388=CARTESIAN_POINT ( 'NONE',  ( 24.90181682663759943, 34.66060904161630418, -136.0552959530562021 ) ) ;
#18391=ORIENTED_EDGE ( 'NONE', *, *, #7638, .T. ) ;
#18409=CARTESIAN_POINT ( 'NONE',  ( -2.499999999969999998, 34.00000000000000000, -136.5552959530000123 ) ) ;
#18444=VECTOR ( 'NONE', #19407, 1000.000000000000000 ) ;
#18460=DIRECTION ( 'NONE',  ( 0.000000000000000000, 1.000000000000000000, 0.000000000000000000 ) ) ;
#18468=LINE ( 'NONE', #4073, #6534 ) ;
#18485=CARTESIAN_POINT ( 'NONE',  ( -32.50000000000000000, -51.50000000000000000, -137.0552959530000123 ) ) ;
#18488=AXIS2_PLACEMENT_3D ( 'NONE', #2923, #13748, #21012 ) ;
#18494=CARTESIAN_POINT ( 'NONE',  ( 11.45511797039051061, 26.15112731430704684, -136.0552959530258761 ) ) ;
#18497=PLANE ( 'NONE',  #16344 ) ;
#18504=CARTESIAN_POINT ( 'NONE',  ( 31.50000000000000000, 40.03620104880000241, -136.0552959530000123 ) ) ;
#18518=ORIENTED_EDGE ( 'NONE', *, *, #22617, .T. ) ;
#18522=DIRECTION ( 'NONE',  ( -2.257144641399999941E-12, 0.000000000000000000, -1.000000000000000000 ) ) ;
#18526=EDGE_CURVE ( 'NONE', #13267, #683, #11947, .T. ) ;
#18560=FACE_OUTER_BOUND ( 'NONE', #14564, .T. ) ;
#18563=DIRECTION ( 'NONE',  ( -1.000000000000000000, 5.094701932209999624E-24, 0.000000000000000000 ) ) ;
#18626=ADVANCED_FACE ( 'NONE', ( #6652 ), #22854, .F. ) ;
#18627=ORIENTED_EDGE ( 'NONE', *, *, #1285, .T. ) ;
#18628=CARTESIAN_POINT ( 'NONE',  ( 14.00000000004000356, 19.51825229575318588, -136.0552959530169517 ) ) ;
#18633=PLANE ( 'NONE',  #13952 ) ;
#18643=FACE_OUTER_BOUND ( 'NONE', #3669, .T. ) ;
#18660=DIRECTION ( 'NONE',  ( 5.094701932209999624E-24, 1.000000000000000000, 0.000000000000000000 ) ) ;
#18663=VECTOR ( 'NONE', #23408, 1000.000000000000000 ) ;
#18664=VERTEX_POINT ( 'NONE', #17256 ) ;
#18676=VERTEX_POINT ( 'NONE', #21784 ) ;
#18692=CARTESIAN_POINT ( 'NONE',  ( -2.489991676528331865, 46.24652334969331946, -136.0552959529943848 ) ) ;
#18698=CARTESIAN_POINT ( 'NONE',  ( 4.500000000009999113, -2.000000000000000000, -136.0552959530000123 ) ) ;
#18699=CARTESIAN_POINT ( 'NONE',  ( 3.611688725869999975E-11, -50.50000000000000000, -136.0552959530000123 ) ) ;
#18715=EDGE_CURVE ( 'NONE', #10697, #22598, #7009, .T. ) ;
#18733=CARTESIAN_POINT ( 'NONE',  ( 4.109320143298619499, -4.961756220215326252, -136.0552959530092778 ) ) ;
#18734=EDGE_LOOP ( 'NONE', ( #23156, #22239, #6320, #2298, #18518, #89, #13703, #11040 ) ) ;
#18743=LINE ( 'NONE', #4454, #10627 ) ;
#18748=FACE_BOUND ( 'NONE', #5307, .T. ) ;
#18763=ORIENTED_EDGE ( 'NONE', *, *, #3128, .T. ) ;
#18787=VERTEX_POINT ( 'NONE', #1435 ) ;
#18792=CARTESIAN_POINT ( 'NONE',  ( 20.50000000000000000, 22.50000000000000000, -136.0552959530000123 ) ) ;
#18799=CARTESIAN_POINT ( 'NONE',  ( -15.92012808077673469, -44.20103055062003961, -136.0552959529640873 ) ) ;
#18808=ORIENTED_EDGE ( 'NONE', *, *, #15155, .T. ) ;
#18810=EDGE_CURVE ( 'NONE', #20903, #15726, #12241, .T. ) ;
#18834=ADVANCED_FACE ( 'NONE', ( #8136 ), #4465, .T. ) ;
#18838=LINE ( 'NONE', #17046, #20802 ) ;
#18846=CARTESIAN_POINT ( 'NONE',  ( 8.750000000030000891, -2.273736754430000208E-12, -136.0552959530000123 ) ) ;
#18848=CARTESIAN_POINT ( 'NONE',  ( -6.366307851350000213, -50.50000000000000000, -137.0552959530000123 ) ) ;
#18852=PLANE ( 'NONE',  #2310 ) ;
#18853=ORIENTED_EDGE ( 'NONE', *, *, #8377, .F. ) ;
#18854=CARTESIAN_POINT ( 'NONE',  ( 13.80479507505236825, 18.53689086730539515, -136.0552959530164969 ) ) ;
#18864=ORIENTED_EDGE ( 'NONE', *, *, #20251, .T. ) ;
#18872=ORIENTED_EDGE ( 'NONE', *, *, #8617, .T. ) ;
#18875=DIRECTION ( 'NONE',  ( 1.000000000000000000, -5.094701932209999624E-24, -2.257144641399999941E-12 ) ) ;
#18887=ORIENTED_EDGE ( 'NONE', *, *, #4487, .F. ) ;
#18908=ORIENTED_EDGE ( 'NONE', *, *, #127, .F. ) ;
#18913=DIRECTION ( 'NONE',  ( 0.000000000000000000, -1.000000000000000000, 0.000000000000000000 ) ) ;
#18915=CARTESIAN_POINT ( 'NONE',  ( -16.46194989540135367, -43.39058393986235984, -136.0552959529628083 ) ) ;
#18925=CARTESIAN_POINT ( 'NONE',  ( 15.50000000000000000, 33.50000000000000000, -136.5552959530000123 ) ) ;
#18933=PLANE ( 'NONE',  #5661 ) ;
#18937=ORIENTED_EDGE ( 'NONE', *, *, #4304, .F. ) ;
#18942=ORIENTED_EDGE ( 'NONE', *, *, #1669, .F. ) ;
#18947=ORIENTED_EDGE ( 'NONE', *, *, #9531, .T. ) ;
#18970=DIRECTION ( 'NONE',  ( -2.257144641399999941E-12, 8.049635416090000264E-35, -1.000000000000000000 ) ) ;
#18983=EDGE_CURVE ( 'NONE', #1242, #4356, #10285, .T. ) ;
#18987=FACE_OUTER_BOUND ( 'NONE', #15308, .T. ) ;
#18997=EDGE_CURVE ( 'NONE', #13875, #10751, #3270, .T. ) ;
#19000=EDGE_CURVE ( 'NONE', #20206, #5119, #15838, .T. ) ;
#19021=VERTEX_POINT ( 'NONE', #4585 ) ;
#19044=CARTESIAN_POINT ( 'NONE',  ( -15.92022845431896982, -41.79886907580737443, -136.0552959529640589 ) ) ;
#19046=LINE ( 'NONE', #13335, #22622 ) ;
#19051=ADVANCED_FACE ( 'NONE', ( #15876 ), #23146, .T. ) ;
#19053=ORIENTED_EDGE ( 'NONE', *, *, #16635, .T. ) ;
#19062=DIRECTION ( 'NONE',  ( 1.000000000000000000, 0.000000000000000000, -2.257453483404485639E-12 ) ) ;
#19068=COLOUR_RGB ( '', 0.08235294, 0.09019608, 0.10196078) ;
#19079=B_SPLINE_CURVE_WITH_KNOTS ( 'NONE', 3,
 ( #18122, #14200, #17889, #21933, #12392, #20150, #15983, #7049, #1606, #3844, #12639, #8940, #8825, #16104, #7167, #10839, #19798, #16219 ),
 .UNSPECIFIED., .F., .F.,
 ( 4, 2, 2, 2, 2, 2, 2, 2, 4 ),
 ( 0.000000000000000000, 0.1250000000000000000, 0.2500000000000000000, 0.3750000000000000000, 0.5000000000000000000, 0.6250000000000000000, 0.7500000000000000000, 0.8750000000000000000, 1.000000000000000000 ),
 .UNSPECIFIED. ) ;
#19082=VERTEX_POINT ( 'NONE', #12892 ) ;
#19090=EDGE_LOOP ( 'NONE', ( #11358, #6518, #21789, #181 ) ) ;
#19093=ORIENTED_EDGE ( 'NONE', *, *, #2257, .F. ) ;
#19102=ORIENTED_EDGE ( 'NONE', *, *, #524, .T. ) ;
#19125=DIRECTION ( 'NONE',  ( 5.094701932209999624E-24, 1.000000000000000000, 0.000000000000000000 ) ) ;
#19128=EDGE_CURVE ( 'NONE', #16693, #6748, #12028, .T. ) ;
#19131=EDGE_LOOP ( 'NONE', ( #23452, #16872, #12649, #921 ) ) ;
#19132=CARTESIAN_POINT ( 'NONE',  ( 1.133692148650000009, -51.50000000000000000, -136.5552959530000123 ) ) ;
#19135=ORIENTED_EDGE ( 'NONE', *, *, #8959, .T. ) ;
#19138=ORIENTED_EDGE ( 'NONE', *, *, #9734, .F. ) ;
#19140=FACE_OUTER_BOUND ( 'NONE', #14761, .T. ) ;
#19147=VERTEX_POINT ( 'NONE', #16580 ) ;
#19161=CARTESIAN_POINT ( 'NONE',  ( -15.39058393985465223, -41.53805010459524283, -136.0552959529652242 ) ) ;
#19166=CARTESIAN_POINT ( 'NONE',  ( 4.500000000009999113, -2.000000000000000000, -136.5552959530000123 ) ) ;
#19173=CARTESIAN_POINT ( 'NONE',  ( 23.00000000000000000, 19.50000000000000000, -137.0552959530000123 ) ) ;
#19185=DIRECTION ( 'NONE',  ( -1.000000000000000000, 0.000000000000000000, 2.254788948169999945E-12 ) ) ;
#19188=VECTOR ( 'NONE', #18145, 1000.000000000000000 ) ;
#19206=LINE ( 'NONE', #22785, #5936 ) ;
#19208=FACE_BOUND ( 'NONE', #18734, .T. ) ;
#19223=CARTESIAN_POINT ( 'NONE',  ( -0.9999999999639996862, 20.99262443222791319, -136.0552959529977954 ) ) ;
#19247=CARTESIAN_POINT ( 'NONE',  ( 15.50000000000000000, 33.50000000000000000, -136.0552959530000123 ) ) ;
#19252=EDGE_LOOP ( 'NONE', ( #14137, #23075, #21386, #18094 ) ) ;
#19284=ORIENTED_EDGE ( 'NONE', *, *, #19721, .T. ) ;
#19293=LINE ( 'NONE', #19173, #10029 ) ;
#19297=CARTESIAN_POINT ( 'NONE',  ( -7.499999999959999997, 19.50000000000000000, -136.0552959530000123 ) ) ;
#19315=FACE_OUTER_BOUND ( 'NONE', #22672, .T. ) ;
#19325=CARTESIAN_POINT ( 'NONE',  ( 3.000000000010000001, -3.500000000000000000, -136.0552959530000123 ) ) ;
#19337=CARTESIAN_POINT ( 'NONE',  ( -1.752427223251484367, 43.49276203925820283, -136.0552959530039345 ) ) ;
#19341=CARTESIAN_POINT ( 'NONE',  ( -0.9999999999649999971, 20.50000000000000000, -136.5552959530000123 ) ) ;
#19349=DIRECTION ( 'NONE',  ( -1.000000000000000000, 0.000000000000000000, 2.257120985840000117E-12 ) ) ;
#19358=CARTESIAN_POINT ( 'NONE',  ( 31.50000000000000000, -36.53620104879999531, -137.0552959530000123 ) ) ;
#19362=AXIS2_PLACEMENT_3D ( 'NONE', #4762, #13812, #1216 ) ;
#19366=AXIS2_PLACEMENT_3D ( 'NONE', #21740, #5540, #21620 ) ;
#19367=CARTESIAN_POINT ( 'NONE',  ( 5.255428470566348764, -4.810679582531388832, -136.0552959530016892 ) ) ;
#19368=VECTOR ( 'NONE', #14138, 1000.000000000000000 ) ;
#19371=ORIENTED_EDGE ( 'NONE', *, *, #2068, .F. ) ;
#19383=EDGE_CURVE ( 'NONE', #14999, #7495, #18838, .T. ) ;
#19384=EDGE_LOOP ( 'NONE', ( #11991, #11856, #17979, #4358 ) ) ;
#19386=VECTOR ( 'NONE', #11137, 1000.000000000000000 ) ;
#19389=CYLINDRICAL_SURFACE ( 'NONE', #9468, 2.999999999999999112 ) ;
#19397=CARTESIAN_POINT ( 'NONE',  ( 20.50000000000000000, 19.50000000000000000, -136.0552959530000123 ) ) ;
#19405=ORIENTED_EDGE ( 'NONE', *, *, #5961, .F. ) ;
#19407=DIRECTION ( 'NONE',  ( 0.000000000000000000, -1.000000000000000000, 0.000000000000000000 ) ) ;
#19411=DIRECTION ( 'NONE',  ( -2.257144641399999941E-12, 8.049635416090000264E-35, -1.000000000000000000 ) ) ;
#19418=CARTESIAN_POINT ( 'NONE',  ( 32.00000000000000000, 20.96379895120000114, -137.0552959530000123 ) ) ;
#19422=CARTESIAN_POINT ( 'NONE',  ( 14.00000000000000000, 20.50000000000000000, -136.0552959530000123 ) ) ;
#19426=ORIENTED_EDGE ( 'NONE', *, *, #15963, .T. ) ;
#19439=AXIS2_PLACEMENT_3D ( 'NONE', #4661, #11900, #2997 ) ;
#19443=EDGE_CURVE ( 'NONE', #6729, #1522, #21457, .T. ) ;
#19461=CARTESIAN_POINT ( 'NONE',  ( 7.976419552989963080, -46.35121046038157289, -136.0552959530180033 ) ) ;
#19465=DIRECTION ( 'NONE',  ( 2.257144641399999941E-12, -8.049635416090000264E-35, 1.000000000000000000 ) ) ;
#19474=( NAMED_UNIT ( * ) PLANE_ANGLE_UNIT ( ) SI_UNIT ( $, .RADIAN. ) );
#19490=EDGE_CURVE ( 'NONE', #17829, #23163, #15089, .T. ) ;
#19508=LINE ( 'NONE', #951, #21653 ) ;
#19520=PLANE ( 'NONE',  #23374 ) ;
#19524=LINE ( 'NONE', #21790, #2582 ) ;
#19531=PLANE ( 'NONE',  #3486 ) ;
#19532=LINE ( 'NONE', #8800, #6485 ) ;
#19543=FACE_OUTER_BOUND ( 'NONE', #15355, .T. ) ;
#19548=CARTESIAN_POINT ( 'NONE',  ( -15.50000000000000000, 47.50000000000000000, -137.0552959530000123 ) ) ;
#19554=CARTESIAN_POINT ( 'NONE',  ( 7.053444247358170216, -30.74994780906165204, -136.0552959530158716 ) ) ;
#19556=EDGE_CURVE ( 'NONE', #11683, #4666, #15248, .T. ) ;
#19562=DIRECTION ( 'NONE',  ( 0.000000000000000000, 1.000000000000000000, 0.000000000000000000 ) ) ;
#19571=EDGE_CURVE ( 'NONE', #8129, #17769, #20486, .T. ) ;
#19580=ORIENTED_EDGE ( 'NONE', *, *, #13206, .T. ) ;
#19583=( NAMED_UNIT ( * ) SI_UNIT ( $, .STERADIAN. ) SOLID_ANGLE_UNIT ( ) );
#19600=CYLINDRICAL_SURFACE ( 'NONE', #4166, 7.500000000000006217 ) ;
#19604=ORIENTED_EDGE ( 'NONE', *, *, #10061, .F. ) ;
#19623=CARTESIAN_POINT ( 'NONE',  ( -2.499999999969999998, 40.00000000000000000, -137.0552959530000123 ) ) ;
#19631=LINE ( 'NONE', #16182, #9839 ) ;
#19634=CARTESIAN_POINT ( 'NONE',  ( 4.553999924799793320, 13.23986818282720890, -136.0552959530102726 ) ) ;
#19638=LINE ( 'NONE', #10694, #15270 ) ;
#19641=CARTESIAN_POINT ( 'NONE',  ( 7.750000000030000002, -38.98606797749999942, -137.0552959530000123 ) ) ;
#19652=AXIS2_PLACEMENT_3D ( 'NONE', #13619, #19465, #2805 ) ;
#19654=VERTEX_POINT ( 'NONE', #20833 ) ;
#19664=AXIS2_PLACEMENT_3D ( 'NONE', #4269, #16757, #7707 ) ;
#19665=CARTESIAN_POINT ( 'NONE',  ( -7.499999999959999997, 22.50000000000000000, -136.0552959530000123 ) ) ;
#19666=CARTESIAN_POINT ( 'NONE',  ( 9.736704675149560728, -34.16257638424990972, -136.0552959530219823 ) ) ;
#19671=DIRECTION ( 'NONE',  ( 2.257144641399999941E-12, -8.049597179213198935E-35, 1.000000000000000000 ) ) ;
#19678=ORIENTED_EDGE ( 'NONE', *, *, #10355, .T. ) ;
#19680=VECTOR ( 'NONE', #16127, 1000.000000000000000 ) ;
#19693=UNCERTAINTY_MEASURE_WITH_UNIT (LENGTH_MEASURE( 1.000000000000000082E-05 ), #14228, 'distance_accuracy_value', 'NONE');
#19694=EDGE_CURVE ( 'NONE', #8186, #23343, #23089, .T. ) ;
#19706=CARTESIAN_POINT ( 'NONE',  ( 24.33939095838566047, 38.90181682662307594, -136.0552959530549515 ) ) ;
#19713=EDGE_CURVE ( 'NONE', #7623, #8661, #22166, .T. ) ;
#19721=EDGE_CURVE ( 'NONE', #22142, #16387, #19524, .T. ) ;
#19722=VECTOR ( 'NONE', #16408, 1000.000000000000000 ) ;
#19727=CARTESIAN_POINT ( 'NONE',  ( -5.499999999969999109, 44.50000000000000000, -136.5552959530000123 ) ) ;
#19742=CARTESIAN_POINT ( 'NONE',  ( 13.13369214870000157, -51.50000000000000000, -136.5552959530000123 ) ) ;
#19748=DIRECTION ( 'NONE',  ( 0.000000000000000000, -1.000000000000000000, 0.000000000000000000 ) ) ;
#19751=CARTESIAN_POINT ( 'NONE',  ( -12.50000000000000000, -2.273736754430000208E-12, -136.0552959530000123 ) ) ;
#19774=DIRECTION ( 'NONE',  ( 2.257144641397284947E-12, -2.714724913984255017E-24, 1.000000000000000000 ) ) ;
#19778=ORIENTED_EDGE ( 'NONE', *, *, #4558, .T. ) ;
#19781=VECTOR ( 'NONE', #805, 1000.000000000000000 ) ;
#19782=FACE_OUTER_BOUND ( 'NONE', #13642, .T. ) ;
#19789=ORIENTED_EDGE ( 'NONE', *, *, #4226, .T. ) ;
#19791=EDGE_CURVE ( 'NONE', #17461, #15193, #12450, .T. ) ;
#19794=CARTESIAN_POINT ( 'NONE',  ( 4.020454867604463800, -35.03105831636347745, -136.0552959530090789 ) ) ;
#19798=CARTESIAN_POINT ( 'NONE',  ( 20.10199673425611877, 25.50000000000003197, -136.0552959530453450 ) ) ;
#19802=CARTESIAN_POINT ( 'NONE',  ( -7.499999999959999997, 19.50000000000000000, -136.0552959530000123 ) ) ;
#19811=CARTESIAN_POINT ( 'NONE',  ( -15.00000000000000000, -41.50000000000000000, -136.0552959530000123 ) ) ;
#19814=CARTESIAN_POINT ( 'NONE',  ( 31.50000000000000000, 20.96379895120000114, -136.0552959530000123 ) ) ;
#19830=PLANE ( 'NONE',  #19366 ) ;
#19835=DIRECTION ( 'NONE',  ( 2.257144641399999941E-12, -8.049635416090000264E-35, 1.000000000000000000 ) ) ;
#19841=STYLED_ITEM ( 'NONE', ( #4828 ), #16897 ) ;
#19844=VECTOR ( 'NONE', #5993, 1000.000000000000000 ) ;
#19854=CARTESIAN_POINT ( 'NONE',  ( -5.246523349656645685, 45.51000832343145674, -136.0552959529881605 ) ) ;
#19862=VECTOR ( 'NONE', #13800, 1000.000000000000000 ) ;
#19866=VERTEX_POINT ( 'NONE', #5927 ) ;
#19869=EDGE_CURVE ( 'NONE', #11242, #21090, #1055, .T. ) ;
#19877=DIRECTION ( 'NONE',  ( 0.000000000000000000, -1.000000000000000000, 0.000000000000000000 ) ) ;
#19890=CARTESIAN_POINT ( 'NONE',  ( -14.24457152944364680, -44.31067958253138528, -136.0552959530016892 ) ) ;
#19892=EDGE_CURVE ( 'NONE', #18676, #8637, #18325, .T. ) ;
#19893=PLANE ( 'NONE',  #15907 ) ;
#19898=VERTEX_POINT ( 'NONE', #14741 ) ;
#19910=CARTESIAN_POINT ( 'NONE',  ( 1.133692148650000009, 51.50000000000000000, -137.0552959530000123 ) ) ;
#19925=PLANE ( 'NONE',  #2892 ) ;
#19939=CARTESIAN_POINT ( 'NONE',  ( 14.00000000000000000, 20.50000000000000000, -136.0552959530000123 ) ) ;
#19948=DIRECTION ( 'NONE',  ( 0.7071067811865473507, -0.7071067811865477948, -1.595945597898661113E-12 ) ) ;
#19953=ORIENTED_EDGE ( 'NONE', *, *, #10435, .F. ) ;
#19967=VERTEX_POINT ( 'NONE', #15438 ) ;
#19970=ORIENTED_EDGE ( 'NONE', *, *, #8959, .F. ) ;
#19971=EDGE_CURVE ( 'NONE', #5099, #8186, #15687, .T. ) ;
#19974=LINE ( 'NONE', #5101, #3757 ) ;
#19986=ORIENTED_EDGE ( 'NONE', *, *, #4998, .F. ) ;
#19998=SURFACE_SIDE_STYLE ('',( #21797 ) ) ;
#19999=EDGE_CURVE ( 'NONE', #2935, #16387, #22949, .T. ) ;
#20000=CARTESIAN_POINT ( 'NONE',  ( 25.50000000000000000, 25.50000000000000000, -136.0552959530000123 ) ) ;
#20014=B_SPLINE_CURVE_WITH_KNOTS ( 'NONE', 3,
 ( #23281, #6970, #14236, #21500, #19706, #10641, #4227, #2098, #11573, #16483, #11115, #9319, #18388, #16592, #3882, #22195, #1994, #7666 ),
 .UNSPECIFIED., .F., .F.,
 ( 4, 2, 2, 2, 2, 2, 2, 2, 4 ),
 ( 0.000000000000000000, 0.1250000000000000000, 0.2500000000000000000, 0.3750000000000000000, 0.5000000000000000000, 0.6250000000000000000, 0.7500000000000000000, 0.8750000000000000000, 1.000000000000000000 ),
 .UNSPECIFIED. ) ;
#20017=CARTESIAN_POINT ( 'NONE',  ( 25.50000000000000000, 25.50000000000000000, -137.0552959530000123 ) ) ;
#20019=ORIENTED_EDGE ( 'NONE', *, *, #11113, .F. ) ;
#20043=LINE ( 'NONE', #2084, #21531 ) ;
#20048=FACE_OUTER_BOUND ( 'NONE', #22579, .T. ) ;
#20057=CARTESIAN_POINT ( 'NONE',  ( 13.61765588496502843, 22.91567315748345024, -136.0552959530307362 ) ) ;
#20069=PLANE ( 'NONE',  #11264 ) ;
#20070=ORIENTED_EDGE ( 'NONE', *, *, #18715, .F. ) ;
#20078=LINE ( 'NONE', #19727, #15039 ) ;
#20083=CARTESIAN_POINT ( 'NONE',  ( -5.499999999959999997, 44.50000000000000000, -136.0552959530000123 ) ) ;
#20086=VERTEX_POINT ( 'NONE', #23410 ) ;
#20093=VECTOR ( 'NONE', #5652, 1000.000000000000000 ) ;
#20096=AXIS2_PLACEMENT_3D ( 'NONE', #8555, #6552, #13820 ) ;
#20106=VERTEX_POINT ( 'NONE', #3423 ) ;
#20108=EDGE_CURVE ( 'NONE', #6084, #8391, #1302, .T. ) ;
#20111=CARTESIAN_POINT ( 'NONE',  ( 7.750000000030000002, -39.98606797749999942, -137.0552959530000123 ) ) ;
#20121=AXIS2_PLACEMENT_3D ( 'NONE', #3918, #12710, #18660 ) ;
#20129=AXIS2_PLACEMENT_3D ( 'NONE', #17219, #2719, #19125 ) ;
#20137=CARTESIAN_POINT ( 'NONE',  ( 6.000000000010000001, -3.500000000000000000, -136.0552959530000123 ) ) ;
#20143=ORIENTED_EDGE ( 'NONE', *, *, #2440, .T. ) ;
#20150=CARTESIAN_POINT ( 'NONE',  ( 18.09808825521564657, 20.66051412330947556, -136.0552959530408259 ) ) ;
#20154=CARTESIAN_POINT ( 'NONE',  ( -6.719053507368635714, 25.42349012523353480, -136.0552959529848636 ) ) ;
#20156=AXIS2_PLACEMENT_3D ( 'NONE', #8242, #4694, #22778 ) ;
#20157=ORIENTED_EDGE ( 'NONE', *, *, #3854, .F. ) ;
#20169=FACE_OUTER_BOUND ( 'NONE', #21190, .T. ) ;
#20171=LINE ( 'NONE', #15624, #11638 ) ;
#20185=CARTESIAN_POINT ( 'NONE',  ( 25.31684607429999900, 45.26810052439999765, -136.0552959530000123 ) ) ;
#20190=AXIS2_PLACEMENT_3D ( 'NONE', #11616, #1054, #829 ) ;
#20191=VERTEX_POINT ( 'NONE', #1888 ) ;
#20206=VERTEX_POINT ( 'NONE', #9334 ) ;
#20239=VERTEX_POINT ( 'NONE', #11019 ) ;
#20246=CARTESIAN_POINT ( 'NONE',  ( -3.499999999959999997, 44.50000000000000000, -136.0552959530000123 ) ) ;
#20249=DIRECTION ( 'NONE',  ( -5.094701932209999624E-24, -1.000000000000000000, 1.149947916579999802E-35 ) ) ;
#20251=EDGE_CURVE ( 'NONE', #8391, #10751, #16497, .T. ) ;
#20254=EDGE_LOOP ( 'NONE', ( #18627, #11214, #15223, #7752 ) ) ;
#20261=CARTESIAN_POINT ( 'NONE',  ( 4.750000000030000002, -35.98606797749999942, -136.5552959530000123 ) ) ;
#20276=DIRECTION ( 'NONE',  ( -1.000000000000000000, 0.000000000000000000, 2.262368070660000099E-12 ) ) ;
#20278=ORIENTED_EDGE ( 'NONE', *, *, #15963, .F. ) ;
#20296=PLANE ( 'NONE',  #17231 ) ;
#20307=CARTESIAN_POINT ( 'NONE',  ( -0.9999999999639999082, 20.50000000000000000, -136.0552959530000123 ) ) ;
#20317=VECTOR ( 'NONE', #8215, 1000.000000000000000 ) ;
#20320=EDGE_LOOP ( 'NONE', ( #17734, #44, #15381, #1618 ) ) ;
#20350=ORIENTED_EDGE ( 'NONE', *, *, #2461, .F. ) ;
#20354=DIRECTION ( 'NONE',  ( 0.000000000000000000, 1.000000000000000000, 0.000000000000000000 ) ) ;
#20374=ADVANCED_FACE ( 'NONE', ( #18987 ), #15185, .F. ) ;
#20396=LINE ( 'NONE', #4091, #600 ) ;
#20403=ORIENTED_EDGE ( 'NONE', *, *, #9154, .T. ) ;
#20407=ORIENTED_EDGE ( 'NONE', *, *, #4956, .T. ) ;
#20423=ORIENTED_EDGE ( 'NONE', *, *, #19869, .T. ) ;
#20449=ORIENTED_EDGE ( 'NONE', *, *, #10170, .F. ) ;
#20450=EDGE_CURVE ( 'NONE', #7723, #15193, #21253, .T. ) ;
#20452=ADVANCED_FACE ( 'NONE', ( #12193 ), #9176, .T. ) ;
#20455=ORIENTED_EDGE ( 'NONE', *, *, #16809, .T. ) ;
#20461=ORIENTED_EDGE ( 'NONE', *, *, #12376, .T. ) ;
#20466=AXIS2_PLACEMENT_3D ( 'NONE', #11788, #5543, #2217 ) ;
#20468=ORIENTED_EDGE ( 'NONE', *, *, #2859, .T. ) ;
#20471=CARTESIAN_POINT ( 'NONE',  ( 32.50000000000000000, -33.03620104880000241, -136.0552959530000123 ) ) ;
#20475=CARTESIAN_POINT ( 'NONE',  ( -2.979194667878099168, 46.44907581354213733, -136.0552959529933048 ) ) ;
#20477=ADVANCED_FACE ( 'NONE', ( #3841 ), #3274, .T. ) ;
#20486=LINE ( 'NONE', #7850, #16242 ) ;
#20488=CIRCLE ( 'NONE', #3016, 7.499999999999999112 ) ;
#20490=CARTESIAN_POINT ( 'NONE',  ( 12.57650987482442595, 37.28094649261360161, -136.0552959530284056 ) ) ;
#20504=CARTESIAN_POINT ( 'NONE',  ( -1.499999999969999998, 44.50000000000000000, -137.0552959530000123 ) ) ;
#20516=CARTESIAN_POINT ( 'NONE',  ( 3.038050104604336887, -3.890583939891920640, -136.0552959530068904 ) ) ;
#20537=CARTESIAN_POINT ( 'NONE',  ( -3.499999999969999998, 42.50000000000000000, -137.0552959530000123 ) ) ;
#20539=EDGE_LOOP ( 'NONE', ( #4780, #15644, #16970, #17611 ) ) ;
#20551=EDGE_CURVE ( 'NONE', #5119, #4448, #2526, .T. ) ;
#20561=EDGE_CURVE ( 'NONE', #18664, #546, #5643, .T. ) ;
#20563=LINE ( 'NONE', #9477, #1897 ) ;
#20565=ORIENTED_EDGE ( 'NONE', *, *, #1853, .T. ) ;
#20566=MECHANICAL_DESIGN_GEOMETRIC_PRESENTATION_REPRESENTATION('',(#22097),#16393);
#20569=PLANE ( 'NONE',  #19664 ) ;
#20571=ORIENTED_EDGE ( 'NONE', *, *, #99, .F. ) ;
#20577=ORIENTED_EDGE ( 'NONE', *, *, #16399, .T. ) ;
#20580=ORIENTED_EDGE ( 'NONE', *, *, #11857, .F. ) ;
#20582=EDGE_CURVE ( 'NONE', #17829, #13267, #2764, .T. ) ;
#20583=DIRECTION ( 'NONE',  ( 2.257144641399999941E-12, -8.049635416090000264E-35, 1.000000000000000000 ) ) ;
#20585=DIRECTION ( 'NONE',  ( 2.257144641399999941E-12, -8.049736840714550138E-35, 1.000000000000000000 ) ) ;
#20586=EDGE_CURVE ( 'NONE', #19967, #18273, #20838, .T. ) ;
#20593=ORIENTED_EDGE ( 'NONE', *, *, #19971, .T. ) ;
#20596=CARTESIAN_POINT ( 'NONE',  ( -16.30974947700681810, -43.75752630172158320, -136.0552959529631778 ) ) ;
#20606=VECTOR ( 'NONE', #10608, 1000.000000000000000 ) ;
#20615=EDGE_CURVE ( 'NONE', #15302, #11614, #7158, .T. ) ;
#20642=VERTEX_POINT ( 'NONE', #15475 ) ;
#20650=CARTESIAN_POINT ( 'NONE',  ( 11.10910039985186160, 14.50249868201364656, -136.0552959530104147 ) ) ;
#20652=DIRECTION ( 'NONE',  ( 1.000000000000000000, 0.000000000000000000, -2.257144641399999941E-12 ) ) ;
#20705=CARTESIAN_POINT ( 'NONE',  ( -16.49999999999998579, -43.19923223293173464, -136.0552959529627515 ) ) ;
#20726=DIRECTION ( 'NONE',  ( 0.000000000000000000, 1.000000000000000000, 0.000000000000000000 ) ) ;
#20733=ADVANCED_FACE ( 'NONE', ( #16189 ), #15952, .T. ) ;
#20738=LINE ( 'NONE', #6330, #7572 ) ;
#20742=CARTESIAN_POINT ( 'NONE',  ( -25.86630785129999666, -51.00000000000000000, -136.0552959530000123 ) ) ;
#20757=DIRECTION ( 'NONE',  ( 5.094701932209999624E-24, 1.000000000000000000, 0.000000000000000000 ) ) ;
#20759=VECTOR ( 'NONE', #22889, 1000.000000000000000 ) ;
#20762=CARTESIAN_POINT ( 'NONE',  ( 6.500000000040000003, 20.50000000000000000, -136.0552959530000123 ) ) ;
#20768=CARTESIAN_POINT ( 'NONE',  ( -32.50000000000000000, 47.50000000000000000, -137.0552959530000123 ) ) ;
#20775=CARTESIAN_POINT ( 'NONE',  ( 16.13369214859999801, -50.50000000000000000, -136.0552959530000123 ) ) ;
#20779=DIRECTION ( 'NONE',  ( 2.255973186040000320E-12, 0.000000000000000000, 1.000000000000000000 ) ) ;
#20781=CARTESIAN_POINT ( 'NONE',  ( -0.9519686233182992341, 21.48063989304531063, -136.0552959529978523 ) ) ;
#20802=VECTOR ( 'NONE', #8356, 1000.000000000000000 ) ;
#20807=CARTESIAN_POINT ( 'NONE',  ( 22.50000000000000000, 39.50000000000000000, -136.5552959530000123 ) ) ;
#20814=LINE ( 'NONE', #10075, #910 ) ;
#20822=VECTOR ( 'NONE', #9260, 1000.000000000000000 ) ;
#20824=ORIENTED_EDGE ( 'NONE', *, *, #10598, .T. ) ;
#20833=CARTESIAN_POINT ( 'NONE',  ( -7.499999999969999109, 48.50000000000000000, -137.0552959530000123 ) ) ;
#20838=LINE ( 'NONE', #6664, #20855 ) ;
#20850=DIRECTION ( 'NONE',  ( -2.257144641399999941E-12, 8.049635416090000264E-35, -1.000000000000000000 ) ) ;
#20855=VECTOR ( 'NONE', #17733, 1000.000000000000000 ) ;
#20860=AXIS2_PLACEMENT_3D ( 'NONE', #6144, #2361, #7913 ) ;
#20881=AXIS2_PLACEMENT_3D ( 'NONE', #20982, #4673, #21781 ) ;
#20903=VERTEX_POINT ( 'NONE', #3930 ) ;
#20931=AXIS2_PLACEMENT_3D ( 'NONE', #1646, #14479, #19948 ) ;
#20940=CARTESIAN_POINT ( 'NONE',  ( -2.499999999959999997, -2.273736754430000208E-12, -136.0552959530000123 ) ) ;
#20948=ORIENTED_EDGE ( 'NONE', *, *, #15196, .F. ) ;
#20950=CARTESIAN_POINT ( 'NONE',  ( -1.753667363927367884, 45.51009696919515335, -136.0552959529960617 ) ) ;
#20958=PLANE ( 'NONE',  #16700 ) ;
#20960=ORIENTED_EDGE ( 'NONE', *, *, #14487, .F. ) ;
#20961=CARTESIAN_POINT ( 'NONE',  ( -15.75752630172931923, -41.69025052297610756, -136.0552959529644284 ) ) ;
#20970=PLANE ( 'NONE',  #19439 ) ;
#20979=CARTESIAN_POINT ( 'NONE',  ( 1.133692148650000009, 51.50000000000000000, -136.0552959530000123 ) ) ;
#20982=CARTESIAN_POINT ( 'NONE',  ( 4.500000000009999113, -3.500000000000000000, -136.0552959530000123 ) ) ;
#20988=LINE ( 'NONE', #4678, #8950 ) ;
#20999=DIRECTION ( 'NONE',  ( 2.257749542879999954E-12, 0.000000000000000000, 1.000000000000000000 ) ) ;
#21012=DIRECTION ( 'NONE',  ( 5.094701932209999624E-24, 1.000000000000000000, 0.000000000000000000 ) ) ;
#21032=PRODUCT_DEFINITION_FORMATION_WITH_SPECIFIED_SOURCE ( 'ANY', '', #11988, .NOT_KNOWN. ) ;
#21037=CARTESIAN_POINT ( 'NONE',  ( 7.750000000030000002, -2.273736754430000208E-12, -136.0552959530000123 ) ) ;
#21040=CARTESIAN_POINT ( 'NONE',  ( -7.499999999969999109, 19.50000000000000000, -137.0552959530000123 ) ) ;
#21041=ORIENTED_EDGE ( 'NONE', *, *, #16824, .F. ) ;
#21043=ADVANCED_FACE ( 'NONE', ( #19140 ), #2609, .T. ) ;
#21044=LINE ( 'NONE', #8414, #19680 ) ;
#21045=FACE_OUTER_BOUND ( 'NONE', #16759, .T. ) ;
#21053=ORIENTED_EDGE ( 'NONE', *, *, #10355, .F. ) ;
#21058=DIRECTION ( 'NONE',  ( -1.000000000000000000, 0.000000000000000000, 2.257120985840000117E-12 ) ) ;
#21060=CARTESIAN_POINT ( 'NONE',  ( -2.499999999969999998, 34.00000000000000000, -137.0552959530000123 ) ) ;
#21068=ORIENTED_EDGE ( 'NONE', *, *, #16678, .F. ) ;
#21073=CARTESIAN_POINT ( 'NONE',  ( 32.50000000000000000, -2.273736754430000208E-12, -136.0552959530000123 ) ) ;
#21080=CARTESIAN_POINT ( 'NONE',  ( 19.50000000000000000, 51.50000000000000000, -137.0552959530000123 ) ) ;
#21085=CARTESIAN_POINT ( 'NONE',  ( -4.499999999959999109, 37.00000000000000000, -136.0552959530000123 ) ) ;
#21090=VERTEX_POINT ( 'NONE', #23415 ) ;
#21107=EDGE_CURVE ( 'NONE', #9912, #11605, #564, .T. ) ;
#21126=DIRECTION ( 'NONE',  ( -1.000000000000000000, 0.000000000000000000, 2.257018101830000309E-12 ) ) ;
#21130=CARTESIAN_POINT ( 'NONE',  ( 3.611688725869999975E-11, 19.50000000000000000, -136.0552959530000123 ) ) ;
#21134=AXIS2_PLACEMENT_3D ( 'NONE', #22827, #13654, #8289 ) ;
#21140=( NAMED_UNIT ( * ) PLANE_ANGLE_UNIT ( ) SI_UNIT ( $, .RADIAN. ) );
#21144=CARTESIAN_POINT ( 'NONE',  ( 2.742437130648935018, 27.00952979664098308, -136.0552959530062083 ) ) ;
#21147=ORIENTED_EDGE ( 'NONE', *, *, #18997, .T. ) ;
#21156=CARTESIAN_POINT ( 'NONE',  ( -15.00000000000000000, -43.00000000000000000, -137.0552959530000123 ) ) ;
#21158=B_SPLINE_CURVE_WITH_KNOTS ( 'NONE', 1,
 ( #7116, #12815 ),
 .UNSPECIFIED., .F., .F.,
 ( 2, 2 ),
 ( -8.099639781640000535, 8.099639781640000535 ),
 .UNSPECIFIED. ) ;
#21172=EDGE_CURVE ( 'NONE', #8089, #12120, #6142, .T. ) ;
#21175=EDGE_LOOP ( 'NONE', ( #20403, #20143, #11310, #16849 ) ) ;
#21185=DIRECTION ( 'NONE',  ( 0.000000000000000000, -1.000000000000000000, 0.000000000000000000 ) ) ;
#21190=EDGE_LOOP ( 'NONE', ( #10376, #16547, #7166, #5011 ) ) ;
#21195=ORIENTED_EDGE ( 'NONE', *, *, #8235, .F. ) ;
#21196=CARTESIAN_POINT ( 'NONE',  ( 6.500000000040000003, 13.00000000000000000, -136.0552959530000123 ) ) ;
#21198=CARTESIAN_POINT ( 'NONE',  ( -32.50000000000000000, 47.50000000000000000, -136.0552959530000123 ) ) ;
#21201=VERTEX_POINT ( 'NONE', #1034 ) ;
#21215=DIRECTION ( 'NONE',  ( 1.000000000000000000, -5.094701932209999624E-24, -2.257144641399999941E-12 ) ) ;
#21227=VERTEX_POINT ( 'NONE', #8030 ) ;
#21242=AXIS2_PLACEMENT_3D ( 'NONE', #7031, #21687, #18342 ) ;
#21253=LINE ( 'NONE', #19341, #21630 ) ;
#21267=DIRECTION ( 'NONE',  ( -2.257198259660000092E-12, 0.000000000000000000, -1.000000000000000000 ) ) ;
#21271=VECTOR ( 'NONE', #22235, 1000.000000000000000 ) ;
#21274=CARTESIAN_POINT ( 'NONE',  ( 5.960959015012474715, -3.892621826538923191, -136.0552959530033377 ) ) ;
#21278=LINE ( 'NONE', #5195, #18663 ) ;
#21301=LINE ( 'NONE', #6649, #8278 ) ;
#21312=LINE ( 'NONE', #21430, #18444 ) ;
#21352=CARTESIAN_POINT ( 'NONE',  ( 23.50000000000000000, -20.50000000000000000, -137.2152959530000089 ) ) ;
#21362=VECTOR ( 'NONE', #21938, 1000.000000000000000 ) ;
#21364=VECTOR ( 'NONE', #10235, 1000.000000000000000 ) ;
#21373=CARTESIAN_POINT ( 'NONE',  ( -2.270906560010169883, 42.90066631520362250, -136.0552959530027408 ) ) ;
#21380=EDGE_LOOP ( 'NONE', ( #14203, #5126, #527, #6282 ) ) ;
#21386=ORIENTED_EDGE ( 'NONE', *, *, #6482, .F. ) ;
#21394=VECTOR ( 'NONE', #6322, 1000.000000000000000 ) ;
#21397=ORIENTED_EDGE ( 'NONE', *, *, #2717, .T. ) ;
#21400=ORIENTED_EDGE ( 'NONE', *, *, #4786, .F. ) ;
#21401=CARTESIAN_POINT ( 'NONE',  ( -9.999999999969999109, 19.50000000000000000, -137.0552959530000123 ) ) ;
#21415=ORIENTED_EDGE ( 'NONE', *, *, #2283, .T. ) ;
#21430=CARTESIAN_POINT ( 'NONE',  ( 1.133692148650000009, 51.00000000000000000, -137.0552959530000123 ) ) ;
#21437=FACE_OUTER_BOUND ( 'NONE', #4827, .T. ) ;
#21439=ADVANCED_FACE ( 'NONE', ( #23346 ), #21694, .T. ) ;
#21453=CARTESIAN_POINT ( 'NONE',  ( -2.499999999969999998, 37.00000000000000000, -137.0552959530000123 ) ) ;
#21457=LINE ( 'NONE', #17883, #22312 ) ;
#21460=CARTESIAN_POINT ( 'NONE',  ( 3.763193976738810509, -34.16260098204838158, -136.0552959530085388 ) ) ;
#21464=ADVANCED_FACE ( 'NONE', ( #4439 ), #13948, .F. ) ;
#21481=EDGE_CURVE ( 'NONE', #5331, #19967, #13473, .T. ) ;
#21492=SHAPE_REPRESENTATION_RELATIONSHIP ( 'NONE' , 'NONE' ,  #6919, #16897 ) ;
#21500=CARTESIAN_POINT ( 'NONE',  ( 24.01462304345166032, 39.11919234680899393, -136.0552959530542125 ) ) ;
#21529=ORIENTED_EDGE ( 'NONE', *, *, #19443, .F. ) ;
#21531=VECTOR ( 'NONE', #10009, 1000.000000000000000 ) ;
#21546=CARTESIAN_POINT ( 'NONE',  ( -0.9520167400502704824, 19.51924065639803629, -136.0552959529979091 ) ) ;
#21555=DIRECTION ( 'NONE',  ( -1.000000000000000000, 0.000000000000000000, 2.245315044999999693E-12 ) ) ;
#21560=VECTOR ( 'NONE', #4912, 1000.000000000000000 ) ;
#21570=ORIENTED_EDGE ( 'NONE', *, *, #1669, .T. ) ;
#21585=ORIENTED_EDGE ( 'NONE', *, *, #18138, .T. ) ;
#21588=CARTESIAN_POINT ( 'NONE',  ( -4.499932713002730900, 22.10251055751376015, -136.0552959529898374 ) ) ;
#21594=CARTESIAN_POINT ( 'NONE',  ( 19.00000000000000000, 39.50000000000000000, -136.0552959530000123 ) ) ;
#21599=DIRECTION ( 'NONE',  ( 2.257144641397284947E-12, -2.714724913984255017E-24, 1.000000000000000000 ) ) ;
#21608=ORIENTED_EDGE ( 'NONE', *, *, #4674, .T. ) ;
#21610=EDGE_CURVE ( 'NONE', #7733, #23343, #16447, .T. ) ;
#21620=DIRECTION ( 'NONE',  ( -2.257144641399999941E-12, 0.000000000000000000, -1.000000000000000000 ) ) ;
#21624=CARTESIAN_POINT ( 'NONE',  ( 22.00000000000000000, -20.50000000000000000, -137.2152959530000089 ) ) ;
#21630=VECTOR ( 'NONE', #5616, 1000.000000000000000 ) ;
#21637=DIRECTION ( 'NONE',  ( -1.000000000000000000, 0.000000000000000000, 2.262368070660000099E-12 ) ) ;
#21647=ORIENTED_EDGE ( 'NONE', *, *, #14171, .T. ) ;
#21653=VECTOR ( 'NONE', #4746, 1000.000000000000000 ) ;
#21656=CARTESIAN_POINT ( 'NONE',  ( -29.18315392570000100, -50.50000000000000000, -137.0552959530000123 ) ) ;
#21679=AXIS2_PLACEMENT_3D ( 'NONE', #10552, #16170, #7120 ) ;
#21682=CARTESIAN_POINT ( 'NONE',  ( -13.69025052297850742, -42.24247369819922682, -136.0552959529691179 ) ) ;
#21685=LINE ( 'NONE', #9029, #11938 ) ;
#21687=DIRECTION ( 'NONE',  ( 3.552713673710000046E-15, -1.000000000000000000, -8.018988631039999700E-27 ) ) ;
#21692=CARTESIAN_POINT ( 'NONE',  ( 3.190056847791982175, -2.742569615067167010, -136.0552959530071746 ) ) ;
#21694=PLANE ( 'NONE',  #9060 ) ;
#21707=VECTOR ( 'NONE', #16116, 1000.000000000000000 ) ;
#21708=DIRECTION ( 'NONE',  ( -2.257144641399999941E-12, 8.049635416090000264E-35, -1.000000000000000000 ) ) ;
#21713=VERTEX_POINT ( 'NONE', #22613 ) ;
#21722=CIRCLE ( 'NONE', #14098, 3.000000000000000000 ) ;
#21723=DIRECTION ( 'NONE',  ( 1.000000000000000000, 0.000000000000000000, -2.257120985840000117E-12 ) ) ;
#21727=PLANE ( 'NONE',  #14268 ) ;
#21728=FACE_OUTER_BOUND ( 'NONE', #13016, .T. ) ;
#21737=CARTESIAN_POINT ( 'NONE',  ( 13.95201674008816006, 21.48075934359548356, -136.0552959530315604 ) ) ;
#21740=CARTESIAN_POINT ( 'NONE',  ( 1.133692148650000009, 51.00000000000000000, -136.0552959530000123 ) ) ;
#21746=CARTESIAN_POINT ( 'NONE',  ( -13.86630785130000021, 50.50000000000000000, -136.5552959530000123 ) ) ;
#21756=ADVANCED_FACE ( 'NONE', ( #4301 ), #20958, .F. ) ;
#21777=LINE ( 'NONE', #10908, #32 ) ;
#21780=EDGE_CURVE ( 'NONE', #19866, #18293, #1087, .T. ) ;
#21781=DIRECTION ( 'NONE',  ( -0.7071067811865473507, -0.7071067811865476838, 1.591319668629389897E-12 ) ) ;
#21782=ADVANCED_FACE ( 'NONE', ( #2757 ), #15595, .F. ) ;
#21784=CARTESIAN_POINT ( 'NONE',  ( 31.50000000000000000, -33.03620104880000241, -137.0552959530000123 ) ) ;
#21789=ORIENTED_EDGE ( 'NONE', *, *, #6323, .F. ) ;
#21790=CARTESIAN_POINT ( 'NONE',  ( 1.133692148650000009, -2.273736754430000208E-12, -136.0552959530000123 ) ) ;
#21792=CARTESIAN_POINT ( 'NONE',  ( 23.50000000000000000, -20.50000000000000000, -136.0552959530000123 ) ) ;
#21797=SURFACE_STYLE_FILL_AREA ( #23214 ) ;
#21798=PLANE ( 'NONE',  #14457 ) ;
#21820=CARTESIAN_POINT ( 'NONE',  ( 4.204281436816111217, -32.13417682219588301, -136.0552959530095052 ) ) ;
#21823=ORIENTED_EDGE ( 'NONE', *, *, #905, .F. ) ;
#21826=CARTESIAN_POINT ( 'NONE',  ( -4.880807653152064773, 20.98537695657578084, -136.0552959529889847 ) ) ;
#21829=DIRECTION ( 'NONE',  ( 5.094701932209999624E-24, 1.000000000000000000, -1.149947916579999802E-35 ) ) ;
#21838=DIRECTION ( 'NONE',  ( 1.000000000000000000, -5.094701932209999624E-24, 0.000000000000000000 ) ) ;
#21855=ORIENTED_EDGE ( 'NONE', *, *, #5242, .T. ) ;
#21858=PLANE ( 'NONE',  #20466 ) ;
#21860=CYLINDRICAL_SURFACE ( 'NONE', #20931, 2.000000000000001776 ) ;
#21884=CARTESIAN_POINT ( 'NONE',  ( 23.50000000000000000, -20.50000000000000000, -137.0552959530000123 ) ) ;
#21896=EDGE_CURVE ( 'NONE', #15683, #2935, #19631, .T. ) ;
#21899=EDGE_LOOP ( 'NONE', ( #22102, #10551, #1964, #17432, #20350, #8772, #5463, #12494, #20960, #8548, #6947, #12172, #8761, #22401, #6939, #21041, #1158, #5487, #18191, #3547, #17124, #10564, #9694, #165, #20449, #4796, #7427, #8543, #5717, #17702, #20019, #19138 ) ) ;
#21916=EDGE_CURVE ( 'NONE', #4825, #3746, #2035, .T. ) ;
#21931=CARTESIAN_POINT ( 'NONE',  ( 15.50000000000000000, 33.50000000000000000, -136.0552959530000123 ) ) ;
#21933=CARTESIAN_POINT ( 'NONE',  ( 18.98537695664905556, 19.88080765317965870, -136.0552959530428438 ) ) ;
#21936=VECTOR ( 'NONE', #2140, 1000.000000000000000 ) ;
#21938=DIRECTION ( 'NONE',  ( 2.257749542879999954E-12, 0.000000000000000000, 1.000000000000000000 ) ) ;
#21948=DIRECTION ( 'NONE',  ( -0.7071067811865463515, -0.7071067811865487940, 1.591319668629388887E-12 ) ) ;
#21957=EDGE_CURVE ( 'NONE', #1756, #17032, #14522, .T. ) ;
#21968=FACE_BOUND ( 'NONE', #15080, .T. ) ;
#21981=EDGE_CURVE ( 'NONE', #4774, #14839, #9258, .T. ) ;
#21987=VERTEX_POINT ( 'NONE', #22471 ) ;
#21997=AXIS2_PLACEMENT_3D ( 'NONE', #1222, #19411, #4534 ) ;
#22004=ADVANCED_FACE ( 'NONE', ( #21045 ), #11500, .T. ) ;
#22007=CARTESIAN_POINT ( 'NONE',  ( 7.750000000030000002, -39.98606797749999942, -136.5552959530000123 ) ) ;
#22064=ADVANCED_FACE ( 'NONE', ( #16987 ), #22586, .T. ) ;
#22082=CARTESIAN_POINT ( 'NONE',  ( -3.499999999969999998, 46.50000000000000000, -137.0552959530000123 ) ) ;
#22083=CARTESIAN_POINT ( 'NONE',  ( -3.499999999969999998, 44.50000000000000000, -137.0552959530000123 ) ) ;
#22089=CARTESIAN_POINT ( 'NONE',  ( 7.133692148649999787, 51.50000000000000000, -137.0552959530000123 ) ) ;
#22097=STYLED_ITEM ( 'NONE', ( #8798 ), #12179 ) ;
#22100=ORIENTED_EDGE ( 'NONE', *, *, #16079, .T. ) ;
#22102=ORIENTED_EDGE ( 'NONE', *, *, #4956, .F. ) ;
#22113=ORIENTED_EDGE ( 'NONE', *, *, #7072, .T. ) ;
#22141=CARTESIAN_POINT ( 'NONE',  ( -4.510008323386228923, 42.75347665030084698, -136.0552959529897805 ) ) ;
#22142=VERTEX_POINT ( 'NONE', #15329 ) ;
#22158=CARTESIAN_POINT ( 'NONE',  ( 12.50006728700867242, 36.10251055748447158, -136.0552959530282351 ) ) ;
#22160=EDGE_CURVE ( 'NONE', #16039, #20239, #14133, .T. ) ;
#22164=CARTESIAN_POINT ( 'NONE',  ( 1.133692148650000009, -51.50000000000000000, -137.0552959530000123 ) ) ;
#22165=EDGE_CURVE ( 'NONE', #21090, #1387, #21278, .T. ) ;
#22166=B_SPLINE_CURVE_WITH_KNOTS ( 'NONE', 3,
 ( #13689, #15361, #22615, #1089, #8319, #19044, #20961, #19161, #5003, #1919 ),
 .UNSPECIFIED., .F., .F.,
 ( 4, 2, 2, 2, 4 ),
 ( 0.000000000000000000, 0.2500000000000000000, 0.5000000000000000000, 0.7500000000000000000, 1.000000000000000000 ),
 .UNSPECIFIED. ) ;
#22169=B_SPLINE_CURVE_WITH_KNOTS ( 'NONE', 3,
 ( #17862, #23447, #17736, #9026, #16311, #1451, #21682, #21, #8672, #12727 ),
 .UNSPECIFIED., .F., .F.,
 ( 4, 2, 2, 2, 4 ),
 ( 0.000000000000000000, 0.2500000000000000000, 0.5000000000000000000, 0.7500000000000000000, 1.000000000000000000 ),
 .UNSPECIFIED. ) ;
#22191=DIRECTION ( 'NONE',  ( 0.000000000000000000, 1.000000000000000000, 0.000000000000000000 ) ) ;
#22195=CARTESIAN_POINT ( 'NONE',  ( 23.28059818845588680, 33.57621958799325768, -136.0552959530525641 ) ) ;
#22196=CARTESIAN_POINT ( 'NONE',  ( 23.00000000000000000, 25.50000000000000000, -136.0552959530000123 ) ) ;
#22204=DIRECTION ( 'NONE',  ( 2.257749542879999954E-12, 0.000000000000000000, 1.000000000000000000 ) ) ;
#22205=DIRECTION ( 'NONE',  ( 1.000000000000000000, -5.094701932209999624E-24, -2.257144641399999941E-12 ) ) ;
#22228=CARTESIAN_POINT ( 'NONE',  ( 14.00000000000000000, 20.50000000000000000, -137.0552959530000123 ) ) ;
#22231=ORIENTED_EDGE ( 'NONE', *, *, #1285, .F. ) ;
#22235=DIRECTION ( 'NONE',  ( 2.255973186040000320E-12, 0.000000000000000000, 1.000000000000000000 ) ) ;
#22239=ORIENTED_EDGE ( 'NONE', *, *, #127, .T. ) ;
#22270=CARTESIAN_POINT ( 'NONE',  ( 14.71905350744857444, 33.57650987476316828, -136.0552959530332373 ) ) ;
#22285=LINE ( 'NONE', #16463, #17906 ) ;
#22290=CARTESIAN_POINT ( 'NONE',  ( 22.00000000000000000, -20.50000000000000000, -136.0552959530000123 ) ) ;
#22305=CARTESIAN_POINT ( 'NONE',  ( -15.50000000000000000, 47.50000000000000000, -136.0552959530000123 ) ) ;
#22309=VECTOR ( 'NONE', #15904, 1000.000000000000000 ) ;
#22312=VECTOR ( 'NONE', #7043, 1000.000000000000000 ) ;
#22313=CYLINDRICAL_SURFACE ( 'NONE', #10082, 1.500000000000001110 ) ;
#22317=EDGE_CURVE ( 'NONE', #19654, #12078, #4112, .T. ) ;
#22337=CARTESIAN_POINT ( 'NONE',  ( -25.86630785129999666, -50.50000000000000000, -136.0552959530000123 ) ) ;
#22361=ORIENTED_EDGE ( 'NONE', *, *, #21896, .T. ) ;
#22366=EDGE_LOOP ( 'NONE', ( #8105, #3100, #15857, #23432 ) ) ;
#22383=DIRECTION ( 'NONE',  ( -1.000000000000000000, 0.000000000000000000, 2.257120985840000117E-12 ) ) ;
#22388=DIRECTION ( 'NONE',  ( 1.000000000000000000, 0.000000000000000000, -2.273736754430000208E-12 ) ) ;
#22396=DIRECTION ( 'NONE',  ( -2.257144641399999941E-12, 8.049635416090000264E-35, -1.000000000000000000 ) ) ;
#22401=ORIENTED_EDGE ( 'NONE', *, *, #15768, .F. ) ;
#22405=AXIS2_PLACEMENT_3D ( 'NONE', #12493, #19774, #10704 ) ;
#22428=DIRECTION ( 'NONE',  ( 2.257157423930000049E-12, 0.000000000000000000, 1.000000000000000000 ) ) ;
#22433=CARTESIAN_POINT ( 'NONE',  ( 3.611450600040000189E-11, -2.273736754430000208E-12, -136.0552959530000123 ) ) ;
#22435=CARTESIAN_POINT ( 'NONE',  ( -29.18315392570000100, -50.50000000000000000, -136.0552959530000123 ) ) ;
#22439=CARTESIAN_POINT ( 'NONE',  ( 32.50000000000000000, 32.96379895120000469, -136.0552959530000123 ) ) ;
#22444=EDGE_LOOP ( 'NONE', ( #1980, #21608, #2473, #6607 ) ) ;
#22446=EDGE_CURVE ( 'NONE', #18676, #16549, #18294, .T. ) ;
#22464=CARTESIAN_POINT ( 'NONE',  ( 3.579771545658129828, -2.298869075814014451, -136.0552959530081125 ) ) ;
#22471=CARTESIAN_POINT ( 'NONE',  ( 25.50000000000000000, 19.50000000000000000, -137.0552959530000123 ) ) ;
#22481=ORIENTED_EDGE ( 'NONE', *, *, #22165, .T. ) ;
#22489=ORIENTED_EDGE ( 'NONE', *, *, #608, .F. ) ;
#22517=DIRECTION ( 'NONE',  ( 1.000000000000000000, 0.000000000000000000, -2.257453483404485639E-12 ) ) ;
#22543=DIRECTION ( 'NONE',  ( 1.000000000000000000, 0.000000000000000000, -2.258578509400000305E-12 ) ) ;
#22548=DIRECTION ( 'NONE',  ( 2.256861364460000137E-12, 0.000000000000000000, 1.000000000000000000 ) ) ;
#22554=CARTESIAN_POINT ( 'NONE',  ( 6.500000000030000002, 28.00000000000000000, -136.5552959530000123 ) ) ;
#22555=CARTESIAN_POINT ( 'NONE',  ( 4.500000000009999113, -3.500000000000000000, -136.0552959530000123 ) ) ;
#22579=EDGE_LOOP ( 'NONE', ( #878, #4025, #14926, #7458 ) ) ;
#22586=PLANE ( 'NONE',  #20190 ) ;
#22588=CARTESIAN_POINT ( 'NONE',  ( 8.750000000030000891, -35.98606797749999942, -136.5552959530000123 ) ) ;
#22597=FACE_OUTER_BOUND ( 'NONE', #19131, .T. ) ;
#22598=VERTEX_POINT ( 'NONE', #22439 ) ;
#22600=CARTESIAN_POINT ( 'NONE',  ( -15.50000000000000000, -2.273736754430000208E-12, -136.0552959530000123 ) ) ;
#22601=ORIENTED_EDGE ( 'NONE', *, *, #8799, .F. ) ;
#22613=CARTESIAN_POINT ( 'NONE',  ( 31.50000000000000000, -21.03620104879999886, -136.0552959530000123 ) ) ;
#22615=CARTESIAN_POINT ( 'NONE',  ( -16.46175622020525608, -42.60932014324554018, -136.0552959529628367 ) ) ;
#22617=EDGE_CURVE ( 'NONE', #4666, #20239, #12378, .T. ) ;
#22620=DIRECTION ( 'NONE',  ( 2.257157423930000049E-12, 0.000000000000000000, 1.000000000000000000 ) ) ;
#22622=VECTOR ( 'NONE', #4411, 1000.000000000000000 ) ;
#22640=ORIENTED_EDGE ( 'NONE', *, *, #17951, .F. ) ;
#22648=EDGE_LOOP ( 'NONE', ( #8526, #15330, #19093, #6736 ) ) ;
#22672=EDGE_LOOP ( 'NONE', ( #20157, #4835, #20565, #19789 ) ) ;
#22676=EDGE_LOOP ( 'NONE', ( #17408, #14464, #10635, #12934 ) ) ;
#22677=PLANE ( 'NONE',  #11764 ) ;
#22688=DIRECTION ( 'NONE',  ( 0.000000000000000000, -1.000000000000000000, 0.000000000000000000 ) ) ;
#22690=CARTESIAN_POINT ( 'NONE',  ( 7.133692148649999787, -51.50000000000000000, -137.0552959530000123 ) ) ;
#22703=LINE ( 'NONE', #20807, #5318 ) ;
#22723=CARTESIAN_POINT ( 'NONE',  ( -9.999999999969999109, 25.50000000000000000, -137.0552959530000123 ) ) ;
#22726=ORIENTED_EDGE ( 'NONE', *, *, #4458, .T. ) ;
#22733=CARTESIAN_POINT ( 'NONE',  ( 15.50000000000000000, 39.50000000000000000, -136.0552959530000123 ) ) ;
#22738=CARTESIAN_POINT ( 'NONE',  ( 25.50000000000000000, 22.50000000000000000, -137.0552959530000123 ) ) ;
#22762=DIRECTION ( 'NONE',  ( -1.000000000000000000, 5.094701932209999624E-24, 0.000000000000000000 ) ) ;
#22775=VECTOR ( 'NONE', #4776, 1000.000000000000000 ) ;
#22778=DIRECTION ( 'NONE',  ( 1.000000000000000000, 0.000000000000000000, -2.262079412673755643E-12 ) ) ;
#22784=EDGE_CURVE ( 'NONE', #23343, #4317, #5852, .T. ) ;
#22785=CARTESIAN_POINT ( 'NONE',  ( -24.00000000000000000, 21.50000000000000000, -137.0552959530000123 ) ) ;
#22789=DIRECTION ( 'NONE',  ( 0.7071067811865473507, -0.7071067811865476838, -1.591319668629389897E-12 ) ) ;
#22790=VECTOR ( 'NONE', #22383, 1000.000000000000000 ) ;
#22800=ORIENTED_EDGE ( 'NONE', *, *, #16227, .T. ) ;
#22804=EDGE_LOOP ( 'NONE', ( #20461, #18908, #10171, #18065 ) ) ;
#22826=EDGE_LOOP ( 'NONE', ( #9309, #14224, #15189, #17580 ) ) ;
#22827=CARTESIAN_POINT ( 'NONE',  ( 6.500000000030000002, 20.50000000000000000, -137.0552959530000123 ) ) ;
#22832=DIRECTION ( 'NONE',  ( -1.000000000000000000, 2.312964634635743450E-15, 2.257453483404485639E-12 ) ) ;
#22852=CIRCLE ( 'NONE', #7251, 3.000000000000000000 ) ;
#22854=CYLINDRICAL_SURFACE ( 'NONE', #13145, 2.000000000000001776 ) ;
#22855=CARTESIAN_POINT ( 'NONE',  ( -32.50000000000000000, 51.50000000000000000, -136.5552959530000123 ) ) ;
#22870=LINE ( 'NONE', #13697, #22775 ) ;
#22871=CARTESIAN_POINT ( 'NONE',  ( 31.50000000000000000, 32.96379895120000469, -136.0552959530000123 ) ) ;
#22878=CARTESIAN_POINT ( 'NONE',  ( -7.499999999969999109, 25.50000000000000000, -136.5552959530000123 ) ) ;
#22889=DIRECTION ( 'NONE',  ( -1.000000000000000000, 0.000000000000000000, 2.258578509400000305E-12 ) ) ;
#22899=ORIENTED_EDGE ( 'NONE', *, *, #57, .T. ) ;
#22902=DIRECTION ( 'NONE',  ( 2.257144641397284947E-12, -2.714724913984255017E-24, 1.000000000000000000 ) ) ;
#22912=DIRECTION ( 'NONE',  ( 0.7071067811865473507, 0.7071067811865477948, -1.595945597898661113E-12 ) ) ;
#22931=ORIENTED_EDGE ( 'NONE', *, *, #21610, .T. ) ;
#22949=LINE ( 'NONE', #19132, #1832 ) ;
#22954=ORIENTED_EDGE ( 'NONE', *, *, #10922, .F. ) ;
#22989=DIRECTION ( 'NONE',  ( -0.7071067811865474617, 0.7071067811865476838, 1.595020412044806951E-12 ) ) ;
#22994=ORIENTED_EDGE ( 'NONE', *, *, #1982, .T. ) ;
#23014=CARTESIAN_POINT ( 'NONE',  ( 4.500000000009999113, -3.500000000000000000, -136.0552959530000123 ) ) ;
#23024=DIRECTION ( 'NONE',  ( 2.257157423930000049E-12, 0.000000000000000000, 1.000000000000000000 ) ) ;
#23032=CARTESIAN_POINT ( 'NONE',  ( 16.13369214859999801, 50.50000000000000000, -136.0552959530000123 ) ) ;
#23034=VECTOR ( 'NONE', #13361, 1000.000000000000000 ) ;
#23042=DIRECTION ( 'NONE',  ( 0.000000000000000000, 1.000000000000000000, 0.000000000000000000 ) ) ;
#23053=CARTESIAN_POINT ( 'NONE',  ( 6.000000000010001777, -3.696349540849364512, -136.0552959530033945 ) ) ;
#23057=EDGE_CURVE ( 'NONE', #21227, #10304, #19638, .T. ) ;
#23075=ORIENTED_EDGE ( 'NONE', *, *, #1525, .F. ) ;
#23082=EDGE_CURVE ( 'NONE', #21713, #15726, #3578, .T. ) ;
#23089=LINE ( 'NONE', #18925, #5618 ) ;
#23091=PLANE ( 'NONE',  #7239 ) ;
#23129=AXIS2_PLACEMENT_3D ( 'NONE', #22083, #877, #15376 ) ;
#23146=PLANE ( 'NONE',  #18488 ) ;
#23156=ORIENTED_EDGE ( 'NONE', *, *, #17217, .T. ) ;
#23160=LINE ( 'NONE', #17927, #6499 ) ;
#23163=VERTEX_POINT ( 'NONE', #16644 ) ;
#23174=ORIENTED_EDGE ( 'NONE', *, *, #5961, .T. ) ;
#23194=DIRECTION ( 'NONE',  ( 1.000000000000000000, 0.000000000000000000, -2.257453483404482811E-12 ) ) ;
#23198=CARTESIAN_POINT ( 'NONE',  ( -32.50000000000000000, -14.50000000000000000, -137.0552959530000123 ) ) ;
#23214=FILL_AREA_STYLE ('',( #14641 ) ) ;
#23229=PLANE ( 'NONE',  #3030 ) ;
#23241=CARTESIAN_POINT ( 'NONE',  ( 4.579308732397330495, -31.65724429029226883, -136.0552959530103294 ) ) ;
#23252=CARTESIAN_POINT ( 'NONE',  ( -13.86630785130000021, -2.273736754430000208E-12, -136.0552959530000123 ) ) ;
#23257=CARTESIAN_POINT ( 'NONE',  ( 25.50000000000000000, 19.50000000000000000, -136.5552959530000123 ) ) ;
#23264=CARTESIAN_POINT ( 'NONE',  ( -2.492762039218201497, 42.75242722329147682, -136.0552959530022861 ) ) ;
#23267=ORIENTED_EDGE ( 'NONE', *, *, #19971, .F. ) ;
#23271=VECTOR ( 'NONE', #14262, 1000.000000000000000 ) ;
#23277=ADVANCED_FACE ( 'NONE', ( #8171 ), #17117, .F. ) ;
#23281=CARTESIAN_POINT ( 'NONE',  ( 22.50000000000000000, 39.50000000000000000, -136.0552959530000123 ) ) ;
#23318=CARTESIAN_POINT ( 'NONE',  ( 25.00000000000000000, -20.50000000000000000, -136.0552959530000123 ) ) ;
#23323=CARTESIAN_POINT ( 'NONE',  ( 1.924189958851657556, 14.53742485369782322, -136.0552959530043324 ) ) ;
#23332=( LENGTH_UNIT ( ) NAMED_UNIT ( * ) SI_UNIT ( .MILLI., .METRE. ) );
#23339=VECTOR ( 'NONE', #10464, 1000.000000000000000 ) ;
#23340=PLANE ( 'NONE',  #21242 ) ;
#23343=VERTEX_POINT ( 'NONE', #19247 ) ;
#23344=FACE_OUTER_BOUND ( 'NONE', #16166, .T. ) ;
#23346=FACE_OUTER_BOUND ( 'NONE', #143, .T. ) ;
#23356=DIRECTION ( 'NONE',  ( -0.7071067811865475727, -0.7071067811865475727, 1.595020412044807153E-12 ) ) ;
#23374=AXIS2_PLACEMENT_3D ( 'NONE', #3214, #10445, #17369 ) ;
#23389=CARTESIAN_POINT ( 'NONE',  ( -32.50000000000000000, -50.50000000000000000, -136.0552959530000123 ) ) ;
#23392=CARTESIAN_POINT ( 'NONE',  ( 8.915777720213307944, 27.61753626548637897, -136.0552959530201065 ) ) ;
#23394=DIRECTION ( 'NONE',  ( 7.105427352510001232E-15, -1.000000000000000000, -1.603797727360000188E-26 ) ) ;
#23406=AXIS2_PLACEMENT_3D ( 'NONE', #16000, #1150, #22912 ) ;
#23408=DIRECTION ( 'NONE',  ( 2.257157423930000049E-12, 0.000000000000000000, 1.000000000000000000 ) ) ;
#23410=CARTESIAN_POINT ( 'NONE',  ( -13.86630785130000021, 51.50000000000000000, -136.0552959530000123 ) ) ;
#23415=CARTESIAN_POINT ( 'NONE',  ( 3.000000000010000001, -3.500000000000000000, -137.0552959530000123 ) ) ;
#23432=ORIENTED_EDGE ( 'NONE', *, *, #22446, .T. ) ;
#23444=DIRECTION ( 'NONE',  ( 1.000000000000000000, -5.094701932209999624E-24, 0.000000000000000000 ) ) ;
#23445=ORIENTED_EDGE ( 'NONE', *, *, #1906, .T. ) ;
#23447=CARTESIAN_POINT ( 'NONE',  ( -14.80113973143733119, -41.50000000000002132, -136.0552959529666168 ) ) ;
#23450=LINE ( 'NONE', #3699, #1716 ) ;
#23452=ORIENTED_EDGE ( 'NONE', *, *, #6482, .T. ) ;
#23471=ADVANCED_FACE ( 'NONE', ( #3085 ), #17594, .T. ) ;
#23479=EDGE_LOOP ( 'NONE', ( #11022, #8340, #22954, #10775 ) ) ;
#23483=ORIENTED_EDGE ( 'NONE', *, *, #18715, .T. ) ;
#23488=VECTOR ( 'NONE', #11128, 1000.000000000000000 ) ;
#23489=LINE ( 'NONE', #5408, #9720 ) ;
#23491=DIRECTION ( 'NONE',  ( 0.000000000000000000, -1.000000000000000000, 0.000000000000000000 ) ) ;
#23504=EDGE_LOOP ( 'NONE', ( #21529, #16688, #9852, #14210 ) ) ;
#23512=PLANE ( 'NONE',  #12129 ) ;
#23517=VERTEX_POINT ( 'NONE', #13626 ) ;
#23518=FACE_BOUND ( 'NONE', #12030, .T. ) ;
#23532=ORIENTED_EDGE ( 'NONE', *, *, #18385, .T. ) ;
#23534=ORIENTED_EDGE ( 'NONE', *, *, #16809, .F. ) ;
#23536=CARTESIAN_POINT ( 'NONE',  ( -5.449075813509844934, 45.02080533206359547, -136.0552959529877342 ) ) ;
ENDSEC;
END-ISO-10303-21;
